ISO-10303-21;
HEADER;
/* Generated by software containing ST-Developer
 * from STEP Tools, Inc. (www.steptools.com) 
 */

FILE_DESCRIPTION(
/* description */ (''),
/* implementation_level */ '2;1');

FILE_NAME(
/* name */ '14_Quill_Guide_Screw_ISO_4028_M8x20_Dog_Point.step',
/* time_stamp */ '2026-10-26T03:50:32-07:00',
/* author */ (''),
/* organization */ (''),
/* preprocessor_version */ 'ST-DEVELOPER v20.2',
/* originating_system */ 'Autodesk Translation Framework v15.15.0.0',
/* authorisation */ '');

FILE_SCHEMA (('AUTOMOTIVE_DESIGN { 1 0 10303 214 3 1 1 }'));
ENDSEC;

DATA;
#10=MECHANICAL_DESIGN_GEOMETRIC_PRESENTATION_REPRESENTATION('',(#1051),#76660);
#164=B_SPLINE_SURFACE_WITH_KNOTS('',3,3,((#57090,#57091,#57092,#57093,#57094,
#57095,#57096,#57097,#57098,#57099,#57100,#57101,#57102,#57103,#57104,#57105,
#57106,#57107,#57108,#57109,#57110,#57111,#57112,#57113,#57114,#57115,#57116,
#57117,#57118,#57119,#57120,#57121,#57122,#57123,#57124,#57125,#57126,#57127,
#57128,#57129,#57130,#57131,#57132,#57133,#57134,#57135,#57136,#57137,#57138,
#57139,#57140,#57141,#57142,#57143,#57144,#57145,#57146,#57147,#57148,#57149,
#57150,#57151,#57152,#57153,#57154,#57155,#57156,#57157,#57158,#57159,#57160,
#57161,#57162,#57163,#57164,#57165,#57166,#57167,#57168,#57169,#57170,#57171,
#57172,#57173,#57174,#57175,#57176,#57177,#57178,#57179,#57180,#57181,#57182),
(#57183,#57184,#57185,#57186,#57187,#57188,#57189,#57190,#57191,#57192,
#57193,#57194,#57195,#57196,#57197,#57198,#57199,#57200,#57201,#57202,#57203,
#57204,#57205,#57206,#57207,#57208,#57209,#57210,#57211,#57212,#57213,#57214,
#57215,#57216,#57217,#57218,#57219,#57220,#57221,#57222,#57223,#57224,#57225,
#57226,#57227,#57228,#57229,#57230,#57231,#57232,#57233,#57234,#57235,#57236,
#57237,#57238,#57239,#57240,#57241,#57242,#57243,#57244,#57245,#57246,#57247,
#57248,#57249,#57250,#57251,#57252,#57253,#57254,#57255,#57256,#57257,#57258,
#57259,#57260,#57261,#57262,#57263,#57264,#57265,#57266,#57267,#57268,#57269,
#57270,#57271,#57272,#57273,#57274,#57275),(#57276,#57277,#57278,#57279,
#57280,#57281,#57282,#57283,#57284,#57285,#57286,#57287,#57288,#57289,#57290,
#57291,#57292,#57293,#57294,#57295,#57296,#57297,#57298,#57299,#57300,#57301,
#57302,#57303,#57304,#57305,#57306,#57307,#57308,#57309,#57310,#57311,#57312,
#57313,#57314,#57315,#57316,#57317,#57318,#57319,#57320,#57321,#57322,#57323,
#57324,#57325,#57326,#57327,#57328,#57329,#57330,#57331,#57332,#57333,#57334,
#57335,#57336,#57337,#57338,#57339,#57340,#57341,#57342,#57343,#57344,#57345,
#57346,#57347,#57348,#57349,#57350,#57351,#57352,#57353,#57354,#57355,#57356,
#57357,#57358,#57359,#57360,#57361,#57362,#57363,#57364,#57365,#57366,#57367,
#57368),(#57369,#57370,#57371,#57372,#57373,#57374,#57375,#57376,#57377,
#57378,#57379,#57380,#57381,#57382,#57383,#57384,#57385,#57386,#57387,#57388,
#57389,#57390,#57391,#57392,#57393,#57394,#57395,#57396,#57397,#57398,#57399,
#57400,#57401,#57402,#57403,#57404,#57405,#57406,#57407,#57408,#57409,#57410,
#57411,#57412,#57413,#57414,#57415,#57416,#57417,#57418,#57419,#57420,#57421,
#57422,#57423,#57424,#57425,#57426,#57427,#57428,#57429,#57430,#57431,#57432,
#57433,#57434,#57435,#57436,#57437,#57438,#57439,#57440,#57441,#57442,#57443,
#57444,#57445,#57446,#57447,#57448,#57449,#57450,#57451,#57452,#57453,#57454,
#57455,#57456,#57457,#57458,#57459,#57460,#57461)),.UNSPECIFIED.,.F.,.F.,
 .F.,(4,4),(4,1,1,1,1,1,1,1,1,1,1,1,1,1,1,1,1,1,1,1,1,1,1,1,1,1,1,1,1,1,
1,1,1,1,1,1,1,1,1,1,1,1,1,1,1,1,1,1,1,1,1,1,1,1,1,1,1,1,1,1,1,1,1,1,1,1,
1,1,1,1,1,1,1,1,1,1,1,1,1,1,1,1,1,1,1,1,1,1,1,1,4),(0.,0.0820126057383863),
(8.31473274985796,9.31317630325708,10.3116198566562,11.3100634100553,12.3085069634544,
13.3069505168535,14.3053940702527,15.3038376236518,16.3022811770509,17.30072473045,
18.2991682838491,19.2976118372482,20.2960553906474,21.2944989440465,22.2929424974456,
23.2913860508447,24.2898296042438,25.2882731576429,26.2867167110421,27.2851602644412,
28.2836038178403,29.2820473712394,30.2804909246385,31.2789344780376,32.2773780314368,
33.2758215848359,34.274265138235,35.2727086916341,36.2711522450332,37.2695957984323,
38.2680393518314,39.2664829052306,40.2649264586297,41.2633700120288,42.2618135654279,
43.260257118827,44.2587006722261,45.2571442256253,46.2555877790244,47.2540313324235,
48.2524748858226,49.2509184392217,50.2493619926208,51.2478055460199,52.2462490994191,
53.2446926528182,54.2431362062173,55.2415797596164,56.2400233130155,57.2384668664147,
58.2369104198138,59.2353539732129,60.233797526612,61.2322410800111,62.2306846334102,
63.2291281868093,64.2275717402085,65.2260152936076,66.2244588470067,67.2229024004058,
68.2213459538049,69.219789507204,70.2182330606032,71.2166766140023,72.2151201674014,
73.2135637208005,74.2120072741996,75.2104508275987,76.2088943809979,77.207337934397,
78.2057814877961,79.2042250411952,80.2026685945943,81.2011121479934,82.1995557013926,
83.1979992547917,84.1964428081908,85.1948863615899,86.193329914989,87.1917734683881,
88.1902170217872,89.1886605751864,90.1871041285855,91.1855476819846,92.1839912353837,
93.1824347887828,94.1808783421819,95.1793218955811,96.1777654489802,97.1762090023793,
98.1746525557784),.UNSPECIFIED.);
#165=B_SPLINE_SURFACE_WITH_KNOTS('',3,3,((#57702,#57703,#57704,#57705,#57706,
#57707,#57708,#57709,#57710,#57711,#57712,#57713,#57714,#57715,#57716,#57717,
#57718,#57719,#57720,#57721,#57722,#57723,#57724,#57725,#57726,#57727,#57728,
#57729,#57730,#57731,#57732,#57733,#57734,#57735,#57736,#57737,#57738,#57739,
#57740,#57741,#57742,#57743,#57744,#57745,#57746,#57747,#57748,#57749,#57750,
#57751,#57752,#57753,#57754,#57755,#57756,#57757,#57758,#57759,#57760,#57761,
#57762,#57763,#57764,#57765,#57766,#57767,#57768,#57769,#57770,#57771,#57772,
#57773,#57774,#57775,#57776,#57777,#57778,#57779,#57780,#57781,#57782,#57783,
#57784,#57785,#57786,#57787,#57788,#57789,#57790,#57791,#57792,#57793,#57794),
(#57795,#57796,#57797,#57798,#57799,#57800,#57801,#57802,#57803,#57804,
#57805,#57806,#57807,#57808,#57809,#57810,#57811,#57812,#57813,#57814,#57815,
#57816,#57817,#57818,#57819,#57820,#57821,#57822,#57823,#57824,#57825,#57826,
#57827,#57828,#57829,#57830,#57831,#57832,#57833,#57834,#57835,#57836,#57837,
#57838,#57839,#57840,#57841,#57842,#57843,#57844,#57845,#57846,#57847,#57848,
#57849,#57850,#57851,#57852,#57853,#57854,#57855,#57856,#57857,#57858,#57859,
#57860,#57861,#57862,#57863,#57864,#57865,#57866,#57867,#57868,#57869,#57870,
#57871,#57872,#57873,#57874,#57875,#57876,#57877,#57878,#57879,#57880,#57881,
#57882,#57883,#57884,#57885,#57886,#57887),(#57888,#57889,#57890,#57891,
#57892,#57893,#57894,#57895,#57896,#57897,#57898,#57899,#57900,#57901,#57902,
#57903,#57904,#57905,#57906,#57907,#57908,#57909,#57910,#57911,#57912,#57913,
#57914,#57915,#57916,#57917,#57918,#57919,#57920,#57921,#57922,#57923,#57924,
#57925,#57926,#57927,#57928,#57929,#57930,#57931,#57932,#57933,#57934,#57935,
#57936,#57937,#57938,#57939,#57940,#57941,#57942,#57943,#57944,#57945,#57946,
#57947,#57948,#57949,#57950,#57951,#57952,#57953,#57954,#57955,#57956,#57957,
#57958,#57959,#57960,#57961,#57962,#57963,#57964,#57965,#57966,#57967,#57968,
#57969,#57970,#57971,#57972,#57973,#57974,#57975,#57976,#57977,#57978,#57979,
#57980),(#57981,#57982,#57983,#57984,#57985,#57986,#57987,#57988,#57989,
#57990,#57991,#57992,#57993,#57994,#57995,#57996,#57997,#57998,#57999,#58000,
#58001,#58002,#58003,#58004,#58005,#58006,#58007,#58008,#58009,#58010,#58011,
#58012,#58013,#58014,#58015,#58016,#58017,#58018,#58019,#58020,#58021,#58022,
#58023,#58024,#58025,#58026,#58027,#58028,#58029,#58030,#58031,#58032,#58033,
#58034,#58035,#58036,#58037,#58038,#58039,#58040,#58041,#58042,#58043,#58044,
#58045,#58046,#58047,#58048,#58049,#58050,#58051,#58052,#58053,#58054,#58055,
#58056,#58057,#58058,#58059,#58060,#58061,#58062,#58063,#58064,#58065,#58066,
#58067,#58068,#58069,#58070,#58071,#58072,#58073)),.UNSPECIFIED.,.F.,.F.,
 .F.,(4,4),(4,1,1,1,1,1,1,1,1,1,1,1,1,1,1,1,1,1,1,1,1,1,1,1,1,1,1,1,1,1,
1,1,1,1,1,1,1,1,1,1,1,1,1,1,1,1,1,1,1,1,1,1,1,1,1,1,1,1,1,1,1,1,1,1,1,1,
1,1,1,1,1,1,1,1,1,1,1,1,1,1,1,1,1,1,1,1,1,1,1,1,4),(0.,0.0820126057383863),
(11.6152142277547,12.6136577811538,13.6121013345529,14.610544887952,15.6089884413511,
16.6074319947502,17.6058755481493,18.6043191015485,19.6027626549476,20.6012062083467,
21.5996497617458,22.5980933151449,23.596536868544,24.5949804219432,25.5934239753423,
26.5918675287414,27.5903110821405,28.5887546355396,29.5871981889387,30.5856417423379,
31.584085295737,32.5825288491361,33.5809724025352,34.5794159559343,35.5778595093334,
36.5763030627326,37.5747466161317,38.5731901695308,39.5716337229299,40.570077276329,
41.5685208297281,42.5669643831273,43.5654079365264,44.5638514899255,45.5622950433246,
46.5607385967237,47.5591821501228,48.557625703522,49.5560692569211,50.5545128103202,
51.5529563637193,52.5513999171184,53.5498434705175,54.5482870239167,55.5467305773158,
56.5451741307149,57.543617684114,58.5420612375131,59.5405047909122,60.5389483443114,
61.5373918977105,62.5358354511096,63.5342790045087,64.5327225579078,65.5311661113069,
66.529609664706,67.5280532181052,68.5264967715043,69.5249403249034,70.5233838783025,
71.5218274317016,72.5202709851007,73.5187145384999,74.517158091899,75.5156016452981,
76.5140451986972,77.5124887520963,78.5109323054954,79.5093758588945,80.5078194122937,
81.5062629656928,82.5047065190919,83.503150072491,84.5015936258901,85.5000371792893,
86.4984807326884,87.4969242860875,88.4953678394866,89.4938113928857,90.4922549462848,
91.4906984996839,92.4891420530831,93.4875856064822,94.4860291598813,95.4844727132804,
96.4829162666795,97.4813598200786,98.4798033734778,99.4782469268769,100.476690480276,
101.475134033675),.UNSPECIFIED.);
#565=B_SPLINE_CURVE_WITH_KNOTS('',3,(#56093,#56094,#56095,#56096,#56097,
#56098,#56099,#56100,#56101,#56102),.UNSPECIFIED.,.F.,.F.,(4,3,3,4),(-4.09274904019424,
-3.99377421359647,-2.99533066019735,-2.06120159751578),.UNSPECIFIED.);
#566=B_SPLINE_CURVE_WITH_KNOTS('',3,(#56105,#56106,#56107,#56108,#56109,
#56110,#56111),.UNSPECIFIED.,.F.,.F.,(4,3,4),(0.,0.998443553399126,1.11004521091126),
 .UNSPECIFIED.);
#567=B_SPLINE_CURVE_WITH_KNOTS('',3,(#56116,#56117,#56118,#56119,#56120,
#56121,#56122,#56123,#56124,#56125,#56126,#56127,#56128,#56129,#56130,#56131,
#56132,#56133,#56134,#56135,#56136,#56137),.UNSPECIFIED.,.F.,.F.,(4,3,3,
3,3,3,3,4),(-10.3759343473738,-9.98443553399116,-8.98599198059205,-7.98754842719293,
-6.98910487379382,-5.9906613203947,-4.99221776699558,-4.09274904019424),
 .UNSPECIFIED.);
#568=B_SPLINE_CURVE_WITH_KNOTS('',3,(#56138,#56139,#56140,#56141,#56142,
#56143,#56144,#56145,#56146,#56147,#56148,#56149,#56150,#56151,#56152,#56153,
#56154,#56155,#56156,#56157,#56158,#56159),.UNSPECIFIED.,.F.,.F.,(4,3,3,
3,3,3,3,4),(1.11004521091126,1.99688710679824,2.99533066019736,3.99377421359647,
4.99221776699558,5.9906613203947,6.98910487379381,7.39323051809085),
 .UNSPECIFIED.);
#569=B_SPLINE_CURVE_WITH_KNOTS('',3,(#56164,#56165,#56166,#56167,#56168,
#56169,#56170,#56171,#56172,#56173,#56174,#56175,#56176,#56177,#56178,#56179,
#56180,#56181,#56182,#56183,#56184,#56185),.UNSPECIFIED.,.F.,.F.,(4,3,3,
3,3,3,3,4),(-16.6591196545534,-15.9750968543859,-14.9766533009867,-13.9782097475876,
-12.9797661941885,-11.9813226407894,-10.9828790873903,-10.3759343473738),
 .UNSPECIFIED.);
#570=B_SPLINE_CURVE_WITH_KNOTS('',3,(#56186,#56187,#56188,#56189,#56190,
#56191,#56192,#56193,#56194,#56195,#56196,#56197,#56198,#56199,#56200,#56201,
#56202,#56203,#56204,#56205,#56206,#56207),.UNSPECIFIED.,.F.,.F.,(4,3,3,
3,3,3,3,4),(7.39323051809085,7.98754842719293,8.98599198059204,9.98443553399115,
10.9828790873903,11.9813226407894,12.9797661941885,13.6764158252704),
 .UNSPECIFIED.);
#571=B_SPLINE_CURVE_WITH_KNOTS('',3,(#56212,#56213,#56214,#56215,#56216,
#56217,#56218,#56219,#56220,#56221,#56222,#56223,#56224,#56225,#56226,#56227,
#56228,#56229,#56230,#56231,#56232,#56233),.UNSPECIFIED.,.F.,.F.,(4,3,3,
3,3,3,3,4),(-22.942304961733,-21.9657581747806,-20.9673146213814,-19.9688710679823,
-18.9704275145832,-17.9719839611841,-16.973540407785,-16.6591196545534),
 .UNSPECIFIED.);
#572=B_SPLINE_CURVE_WITH_KNOTS('',3,(#56234,#56235,#56236,#56237,#56238,
#56239,#56240,#56241,#56242,#56243,#56244,#56245,#56246,#56247,#56248,#56249,
#56250,#56251,#56252,#56253,#56254,#56255),.UNSPECIFIED.,.F.,.F.,(4,3,3,
3,3,3,3,4),(13.6764158252704,13.9782097475876,14.9766533009867,15.9750968543859,
16.973540407785,17.9719839611841,18.9704275145832,19.95960113245),
 .UNSPECIFIED.);
#573=B_SPLINE_CURVE_WITH_KNOTS('',3,(#56260,#56261,#56262,#56263,#56264,
#56265,#56266,#56267,#56268,#56269,#56270,#56271,#56272,#56273,#56274,#56275,
#56276,#56277,#56278,#56279,#56280,#56281,#56282,#56283,#56284),
 .UNSPECIFIED.,.F.,.F.,(4,3,3,3,3,3,3,3,4),(-29.2254902689126,-28.9548630485744,
-27.9564194951753,-26.9579759417761,-25.959532388377,-24.9610888349779,
-23.9626452815788,-22.9642017281797,-22.942304961733),.UNSPECIFIED.);
#574=B_SPLINE_CURVE_WITH_KNOTS('',3,(#56285,#56286,#56287,#56288,#56289,
#56290,#56291,#56292,#56293,#56294,#56295,#56296,#56297,#56298,#56299,#56300,
#56301,#56302,#56303,#56304,#56305,#56306,#56307,#56308,#56309),
 .UNSPECIFIED.,.F.,.F.,(4,3,3,3,3,3,3,3,4),(19.95960113245,19.9688710679823,
20.9673146213814,21.9657581747806,22.9642017281797,23.9626452815788,24.9610888349779,
25.959532388377,26.2427864396296),.UNSPECIFIED.);
#575=B_SPLINE_CURVE_WITH_KNOTS('',3,(#56314,#56315,#56316,#56317,#56318,
#56319,#56320,#56321,#56322,#56323,#56324,#56325,#56326,#56327,#56328,#56329,
#56330,#56331,#56332,#56333,#56334,#56335),.UNSPECIFIED.,.F.,.F.,(4,3,3,
3,3,3,3,4),(-35.5086755760922,-34.9455243689691,-33.94708081557,-32.9486372621708,
-31.9501937087717,-30.9517501553726,-29.9533066019735,-29.2254902689126),
 .UNSPECIFIED.);
#576=B_SPLINE_CURVE_WITH_KNOTS('',3,(#56336,#56337,#56338,#56339,#56340,
#56341,#56342,#56343,#56344,#56345,#56346,#56347,#56348,#56349,#56350,#56351,
#56352,#56353,#56354,#56355,#56356,#56357),.UNSPECIFIED.,.F.,.F.,(4,3,3,
3,3,3,3,4),(26.2427864396296,26.9579759417761,27.9564194951753,28.9548630485744,
29.9533066019735,30.9517501553726,31.9501937087717,32.5259717468092),
 .UNSPECIFIED.);
#577=B_SPLINE_CURVE_WITH_KNOTS('',3,(#56362,#56363,#56364,#56365,#56366,
#56367,#56368,#56369,#56370,#56371,#56372,#56373,#56374,#56375,#56376,#56377,
#56378,#56379,#56380,#56381,#56382,#56383),.UNSPECIFIED.,.F.,.F.,(4,3,3,
3,3,3,3,4),(-41.7918608832718,-40.9361856893638,-39.9377421359646,-38.9392985825655,
-37.9408550291664,-36.9424114757673,-35.9439679223682,-35.5086755760922),
 .UNSPECIFIED.);
#578=B_SPLINE_CURVE_WITH_KNOTS('',3,(#56384,#56385,#56386,#56387,#56388,
#56389,#56390,#56391,#56392,#56393,#56394,#56395,#56396,#56397,#56398,#56399,
#56400,#56401,#56402,#56403,#56404,#56405),.UNSPECIFIED.,.F.,.F.,(4,3,3,
3,3,3,3,4),(32.5259717468092,32.9486372621708,33.9470808155699,34.9455243689691,
35.9439679223682,36.9424114757673,37.9408550291664,38.8091570539888),
 .UNSPECIFIED.);
#579=B_SPLINE_CURVE_WITH_KNOTS('',3,(#56410,#56411,#56412,#56413,#56414,
#56415,#56416,#56417,#56418,#56419,#56420,#56421,#56422,#56423,#56424,#56425,
#56426,#56427,#56428,#56429,#56430,#56431,#56432,#56433,#56434),
 .UNSPECIFIED.,.F.,.F.,(4,3,3,3,3,3,3,3,4),(-48.0750461904514,-47.9252905631576,
-46.9268470097585,-45.9284034563593,-44.9299599029602,-43.9315163495611,
-42.933072796162,-41.9346292427629,-41.7918608832718),.UNSPECIFIED.);
#580=B_SPLINE_CURVE_WITH_KNOTS('',3,(#56435,#56436,#56437,#56438,#56439,
#56440,#56441,#56442,#56443,#56444,#56445,#56446,#56447,#56448,#56449,#56450,
#56451,#56452,#56453,#56454,#56455,#56456,#56457,#56458,#56459),
 .UNSPECIFIED.,.F.,.F.,(4,3,3,3,3,3,3,3,4),(38.8091570539888,38.9392985825655,
39.9377421359646,40.9361856893638,41.9346292427629,42.933072796162,43.9315163495611,
44.9299599029602,45.0923423611684),.UNSPECIFIED.);
#581=B_SPLINE_CURVE_WITH_KNOTS('',3,(#56464,#56465,#56466,#56467,#56468,
#56469,#56470,#56471,#56472,#56473,#56474,#56475,#56476,#56477,#56478,#56479,
#56480,#56481,#56482,#56483,#56484,#56485),.UNSPECIFIED.,.F.,.F.,(4,3,3,
3,3,3,3,4),(-54.358231497631,-53.9159518835523,-52.9175083301532,-51.9190647767541,
-50.9206212233549,-49.9221776699558,-48.9237341165567,-48.0750461904514),
 .UNSPECIFIED.);
#582=B_SPLINE_CURVE_WITH_KNOTS('',3,(#56486,#56487,#56488,#56489,#56490,
#56491,#56492,#56493,#56494,#56495,#56496,#56497,#56498,#56499,#56500,#56501,
#56502,#56503,#56504,#56505,#56506,#56507),.UNSPECIFIED.,.F.,.F.,(4,3,3,
3,3,3,3,4),(45.0923423611684,45.9284034563593,46.9268470097585,47.9252905631576,
48.9237341165567,49.9221776699558,50.9206212233549,51.375527668348),
 .UNSPECIFIED.);
#583=B_SPLINE_CURVE_WITH_KNOTS('',3,(#56512,#56513,#56514,#56515,#56516,
#56517,#56518,#56519,#56520,#56521,#56522,#56523,#56524,#56525,#56526,#56527,
#56528,#56529,#56530,#56531,#56532,#56533),.UNSPECIFIED.,.F.,.F.,(4,3,3,
3,3,3,3,4),(-60.6414168048105,-59.906613203947,-58.9081696505479,-57.9097260971487,
-56.9112825437496,-55.9128389903505,-54.9143954369514,-54.358231497631),
 .UNSPECIFIED.);
#584=B_SPLINE_CURVE_WITH_KNOTS('',3,(#56534,#56535,#56536,#56537,#56538,
#56539,#56540,#56541,#56542,#56543,#56544,#56545,#56546,#56547,#56548,#56549,
#56550,#56551,#56552,#56553,#56554,#56555),.UNSPECIFIED.,.F.,.F.,(4,3,3,
3,3,3,3,4),(51.375527668348,51.919064776754,52.9175083301532,53.9159518835523,
54.9143954369514,55.9128389903505,56.9112825437496,57.6587129755276),
 .UNSPECIFIED.);
#585=B_SPLINE_CURVE_WITH_KNOTS('',3,(#56560,#56561,#56562,#56563,#56564,
#56565,#56566,#56567,#56568,#56569,#56570,#56571,#56572,#56573,#56574,#56575,
#56576,#56577,#56578,#56579,#56580,#56581,#56582,#56583,#56584),
 .UNSPECIFIED.,.F.,.F.,(4,3,3,3,3,3,3,3,4),(-66.9246021119901,-66.8957180777408,
-65.8972745243417,-64.8988309709426,-63.9003874175434,-62.9019438641443,
-61.9035003107452,-60.9050567573461,-60.6414168048105),.UNSPECIFIED.);
#586=B_SPLINE_CURVE_WITH_KNOTS('',3,(#56585,#56586,#56587,#56588,#56589,
#56590,#56591,#56592,#56593,#56594,#56595,#56596,#56597,#56598,#56599,#56600,
#56601,#56602,#56603,#56604,#56605,#56606,#56607,#56608,#56609),
 .UNSPECIFIED.,.F.,.F.,(4,3,3,3,3,3,3,3,4),(57.6587129755276,57.9097260971487,
58.9081696505479,59.906613203947,60.9050567573461,61.9035003107452,62.9019438641443,
63.9003874175434,63.9418982827071),.UNSPECIFIED.);
#587=B_SPLINE_CURVE_WITH_KNOTS('',3,(#56614,#56615,#56616,#56617,#56618,
#56619,#56620,#56621,#56622,#56623,#56624,#56625,#56626,#56627,#56628,#56629,
#56630,#56631,#56632,#56633,#56634,#56635),.UNSPECIFIED.,.F.,.F.,(4,3,3,
3,3,3,3,4),(-73.2077874191697,-72.8863793981355,-71.8879358447363,-70.8894922913372,
-69.8910487379381,-68.892605184539,-67.8941616311399,-66.9246021119901),
 .UNSPECIFIED.);
#588=B_SPLINE_CURVE_WITH_KNOTS('',3,(#56636,#56637,#56638,#56639,#56640,
#56641,#56642,#56643,#56644,#56645,#56646,#56647,#56648,#56649,#56650,#56651,
#56652,#56653,#56654,#56655,#56656,#56657),.UNSPECIFIED.,.F.,.F.,(4,3,3,
3,3,3,3,4),(63.9418982827071,64.8988309709426,65.8972745243417,66.8957180777408,
67.8941616311399,68.892605184539,69.8910487379381,70.2250835898868),
 .UNSPECIFIED.);
#589=B_SPLINE_CURVE_WITH_KNOTS('',3,(#56662,#56663,#56664,#56665,#56666,
#56667,#56668,#56669,#56670,#56671,#56672,#56673,#56674,#56675,#56676,#56677,
#56678,#56679,#56680,#56681,#56682,#56683),.UNSPECIFIED.,.F.,.F.,(4,3,3,
3,3,3,3,4),(-79.4909727263493,-78.8770407185302,-77.8785971651311,-76.8801536117319,
-75.8817100583328,-74.8832665049337,-73.8848229515346,-73.2077874191697),
 .UNSPECIFIED.);
#590=B_SPLINE_CURVE_WITH_KNOTS('',3,(#56684,#56685,#56686,#56687,#56688,
#56689,#56690,#56691,#56692,#56693,#56694,#56695,#56696,#56697,#56698,#56699,
#56700,#56701,#56702,#56703,#56704,#56705),.UNSPECIFIED.,.F.,.F.,(4,3,3,
3,3,3,3,4),(70.2250835898868,70.8894922913372,71.8879358447364,72.8863793981355,
73.8848229515346,74.8832665049337,75.8817100583328,76.5082688970663),
 .UNSPECIFIED.);
#591=B_SPLINE_CURVE_WITH_KNOTS('',3,(#56710,#56711,#56712,#56713,#56714,
#56715,#56716,#56717,#56718,#56719,#56720,#56721,#56722,#56723,#56724,#56725,
#56726,#56727,#56728,#56729,#56730,#56731),.UNSPECIFIED.,.F.,.F.,(4,3,3,
3,3,3,3,4),(-85.7741580335289,-84.8677020389249,-83.8692584855258,-82.8708149321266,
-81.8723713787275,-80.8739278253284,-79.8754842719293,-79.4909727263493),
 .UNSPECIFIED.);
#592=B_SPLINE_CURVE_WITH_KNOTS('',3,(#56732,#56733,#56734,#56735,#56736,
#56737,#56738,#56739,#56740,#56741,#56742,#56743,#56744,#56745,#56746,#56747,
#56748,#56749,#56750,#56751,#56752,#56753),.UNSPECIFIED.,.F.,.F.,(4,3,3,
3,3,3,3,4),(76.5082688970663,76.8801536117319,77.8785971651311,78.8770407185302,
79.8754842719293,80.8739278253284,81.8723713787275,82.7914542042459),
 .UNSPECIFIED.);
#593=B_SPLINE_CURVE_WITH_KNOTS('',3,(#56759,#56760,#56761,#56762,#56763,
#56764),.UNSPECIFIED.,.F.,.F.,(4,1,1,4),(97.3893722612836,97.4813598200786,
98.4798033734778,99.4139324361594),.UNSPECIFIED.);
#594=B_SPLINE_CURVE_WITH_KNOTS('',3,(#56767,#56768,#56769,#56770),
 .UNSPECIFIED.,.F.,.F.,(4,4),(97.3893722612836,98.1746525557784),
 .UNSPECIFIED.);
#595=B_SPLINE_CURVE_WITH_KNOTS('',3,(#56775,#56776,#56777,#56778,#56779,
#56780,#56781,#56782,#56783,#56784),.UNSPECIFIED.,.F.,.F.,(4,1,1,1,1,1,
1,4),(91.106186954104,91.4906984996839,92.4891420530831,93.4875856064822,
94.4860291598813,95.4844727132804,96.4829162666795,97.3893722612836),
 .UNSPECIFIED.);
#596=B_SPLINE_CURVE_WITH_KNOTS('',3,(#56785,#56786,#56787,#56788,#56789,
#56790,#56791,#56792,#56793,#56794,#56795),.UNSPECIFIED.,.F.,.F.,(4,1,1,
1,1,1,1,1,4),(91.106186954104,91.1855476819846,92.1839912353837,93.1824347887828,
94.1808783421819,95.1793218955811,96.1777654489802,97.1762090023793,97.3893722612836),
 .UNSPECIFIED.);
#597=B_SPLINE_CURVE_WITH_KNOTS('',3,(#56800,#56801,#56802,#56803,#56804,
#56805,#56806,#56807,#56808,#56809),.UNSPECIFIED.,.F.,.F.,(4,1,1,1,1,1,
1,4),(84.8230016469244,85.5000371792893,86.4984807326884,87.4969242860875,
88.4953678394866,89.4938113928857,90.4922549462848,91.106186954104),
 .UNSPECIFIED.);
#598=B_SPLINE_CURVE_WITH_KNOTS('',3,(#56810,#56811,#56812,#56813,#56814,
#56815,#56816,#56817,#56818,#56819),.UNSPECIFIED.,.F.,.F.,(4,1,1,1,1,1,
1,4),(84.8230016469244,85.1948863615899,86.193329914989,87.1917734683881,
88.1902170217872,89.1886605751864,90.1871041285855,91.106186954104),
 .UNSPECIFIED.);
#599=B_SPLINE_CURVE_WITH_KNOTS('',3,(#56824,#56825,#56826,#56827,#56828,
#56829,#56830,#56831,#56832,#56833),.UNSPECIFIED.,.F.,.F.,(4,1,1,1,1,1,
1,4),(78.5398163397448,79.5093758588945,80.5078194122937,81.5062629656928,
82.5047065190919,83.503150072491,84.5015936258901,84.8230016469244),
 .UNSPECIFIED.);
#600=B_SPLINE_CURVE_WITH_KNOTS('',3,(#56834,#56835,#56836,#56837,#56838,
#56839,#56840,#56841,#56842,#56843),.UNSPECIFIED.,.F.,.F.,(4,1,1,1,1,1,
1,4),(78.5398163397448,79.2042250411952,80.2026685945943,81.2011121479934,
82.1995557013926,83.1979992547917,84.1964428081908,84.8230016469244),
 .UNSPECIFIED.);
#601=B_SPLINE_CURVE_WITH_KNOTS('',3,(#56848,#56849,#56850,#56851,#56852,
#56853,#56854,#56855,#56856,#56857,#56858),.UNSPECIFIED.,.F.,.F.,(4,1,1,
1,1,1,1,1,4),(72.2566310325652,72.5202709851007,73.5187145384999,74.517158091899,
75.5156016452981,76.5140451986972,77.5124887520963,78.5109323054954,78.5398163397448),
 .UNSPECIFIED.);
#602=B_SPLINE_CURVE_WITH_KNOTS('',3,(#56859,#56860,#56861,#56862,#56863,
#56864,#56865,#56866,#56867,#56868),.UNSPECIFIED.,.F.,.F.,(4,1,1,1,1,1,
1,4),(72.2566310325652,73.2135637208005,74.2120072741996,75.2104508275987,
76.2088943809979,77.207337934397,78.2057814877961,78.5398163397448),
 .UNSPECIFIED.);
#603=B_SPLINE_CURVE_WITH_KNOTS('',3,(#56873,#56874,#56875,#56876,#56877,
#56878,#56879,#56880,#56881,#56882),.UNSPECIFIED.,.F.,.F.,(4,1,1,1,1,1,
1,4),(65.9734457253856,66.529609664706,67.5280532181052,68.5264967715043,
69.5249403249034,70.5233838783025,71.5218274317016,72.2566310325652),
 .UNSPECIFIED.);
#604=B_SPLINE_CURVE_WITH_KNOTS('',3,(#56883,#56884,#56885,#56886,#56887,
#56888,#56889,#56890,#56891,#56892,#56893),.UNSPECIFIED.,.F.,.F.,(4,1,1,
1,1,1,1,1,4),(65.9734457253856,66.2244588470067,67.2229024004058,68.2213459538049,
69.219789507204,70.2182330606032,71.2166766140023,72.2151201674014,72.2566310325652),
 .UNSPECIFIED.);
#605=B_SPLINE_CURVE_WITH_KNOTS('',3,(#56898,#56899,#56900,#56901,#56902,
#56903,#56904,#56905,#56906,#56907),.UNSPECIFIED.,.F.,.F.,(4,1,1,1,1,1,
1,4),(59.690260418206,60.5389483443114,61.5373918977105,62.5358354511096,
63.5342790045087,64.5327225579078,65.5311661113069,65.9734457253856),
 .UNSPECIFIED.);
#606=B_SPLINE_CURVE_WITH_KNOTS('',3,(#56908,#56909,#56910,#56911,#56912,
#56913,#56914,#56915,#56916,#56917),.UNSPECIFIED.,.F.,.F.,(4,1,1,1,1,1,
1,4),(59.690260418206,60.233797526612,61.2322410800111,62.2306846334102,
63.2291281868093,64.2275717402085,65.2260152936076,65.9734457253856),
 .UNSPECIFIED.);
#607=B_SPLINE_CURVE_WITH_KNOTS('',3,(#56922,#56923,#56924,#56925,#56926,
#56927,#56928,#56929,#56930,#56931,#56932),.UNSPECIFIED.,.F.,.F.,(4,1,1,
1,1,1,1,1,4),(53.4070751110264,53.5498434705175,54.5482870239167,55.5467305773158,
56.5451741307149,57.543617684114,58.5420612375131,59.5405047909122,59.690260418206),
 .UNSPECIFIED.);
#608=B_SPLINE_CURVE_WITH_KNOTS('',3,(#56933,#56934,#56935,#56936,#56937,
#56938,#56939,#56940,#56941,#56942),.UNSPECIFIED.,.F.,.F.,(4,1,1,1,1,1,
1,4),(53.4070751110264,54.2431362062173,55.2415797596164,56.2400233130155,
57.2384668664147,58.2369104198138,59.2353539732129,59.690260418206),
 .UNSPECIFIED.);
#609=B_SPLINE_CURVE_WITH_KNOTS('',3,(#56947,#56948,#56949,#56950,#56951,
#56952,#56953,#56954,#56955,#56956),.UNSPECIFIED.,.F.,.F.,(4,1,1,1,1,1,
1,4),(47.1238898038469,47.5591821501228,48.557625703522,49.5560692569211,
50.5545128103202,51.5529563637193,52.5513999171184,53.4070751110264),
 .UNSPECIFIED.);
#610=B_SPLINE_CURVE_WITH_KNOTS('',3,(#56957,#56958,#56959,#56960,#56961,
#56962,#56963,#56964,#56965,#56966,#56967),.UNSPECIFIED.,.F.,.F.,(4,1,1,
1,1,1,1,1,4),(47.1238898038468,47.2540313324235,48.2524748858226,49.2509184392217,
50.2493619926208,51.2478055460199,52.2462490994191,53.2446926528182,53.4070751110264),
 .UNSPECIFIED.);
#611=B_SPLINE_CURVE_WITH_KNOTS('',3,(#56972,#56973,#56974,#56975,#56976,
#56977,#56978,#56979,#56980,#56981),.UNSPECIFIED.,.F.,.F.,(4,1,1,1,1,1,
1,4),(40.8407044966673,41.5685208297281,42.5669643831273,43.5654079365264,
44.5638514899255,45.5622950433246,46.5607385967237,47.1238898038469),
 .UNSPECIFIED.);
#612=B_SPLINE_CURVE_WITH_KNOTS('',3,(#56982,#56983,#56984,#56985,#56986,
#56987,#56988,#56989,#56990,#56991),.UNSPECIFIED.,.F.,.F.,(4,1,1,1,1,1,
1,4),(40.8407044966672,41.2633700120288,42.2618135654279,43.260257118827,
44.2587006722261,45.2571442256253,46.2555877790244,47.1238898038468),
 .UNSPECIFIED.);
#613=B_SPLINE_CURVE_WITH_KNOTS('',3,(#56996,#56997,#56998,#56999,#57000,
#57001,#57002,#57003,#57004,#57005,#57006),.UNSPECIFIED.,.F.,.F.,(4,1,1,
1,1,1,1,1,4),(34.5575191894877,34.5794159559343,35.5778595093334,36.5763030627326,
37.5747466161317,38.5731901695308,39.5716337229299,40.570077276329,40.8407044966673),
 .UNSPECIFIED.);
#614=B_SPLINE_CURVE_WITH_KNOTS('',3,(#57007,#57008,#57009,#57010,#57011,
#57012,#57013,#57014,#57015,#57016),.UNSPECIFIED.,.F.,.F.,(4,1,1,1,1,1,
1,4),(34.5575191894877,35.2727086916341,36.2711522450332,37.2695957984323,
38.2680393518314,39.2664829052306,40.2649264586297,40.8407044966672),
 .UNSPECIFIED.);
#615=B_SPLINE_CURVE_WITH_KNOTS('',3,(#57021,#57022,#57023,#57024,#57025,
#57026,#57027,#57028,#57029,#57030),.UNSPECIFIED.,.F.,.F.,(4,1,1,1,1,1,
1,4),(28.2743338823081,28.5887546355396,29.5871981889387,30.5856417423379,
31.584085295737,32.5825288491361,33.5809724025352,34.5575191894877),
 .UNSPECIFIED.);
#616=B_SPLINE_CURVE_WITH_KNOTS('',3,(#57031,#57032,#57033,#57034,#57035,
#57036,#57037,#57038,#57039,#57040,#57041),.UNSPECIFIED.,.F.,.F.,(4,1,1,
1,1,1,1,1,4),(28.2743338823081,28.2836038178403,29.2820473712394,30.2804909246385,
31.2789344780376,32.2773780314368,33.2758215848359,34.274265138235,34.5575191894877),
 .UNSPECIFIED.);
#617=B_SPLINE_CURVE_WITH_KNOTS('',3,(#57046,#57047,#57048,#57049,#57050,
#57051,#57052,#57053,#57054,#57055),.UNSPECIFIED.,.F.,.F.,(4,1,1,1,1,1,
1,4),(21.9911485751285,22.5980933151449,23.596536868544,24.5949804219432,
25.5934239753423,26.5918675287414,27.5903110821405,28.2743338823081),
 .UNSPECIFIED.);
#618=B_SPLINE_CURVE_WITH_KNOTS('',3,(#57056,#57057,#57058,#57059,#57060,
#57061,#57062,#57063,#57064,#57065),.UNSPECIFIED.,.F.,.F.,(4,1,1,1,1,1,
1,4),(21.9911485751285,22.2929424974456,23.2913860508447,24.2898296042438,
25.2882731576429,26.2867167110421,27.2851602644412,28.2743338823081),
 .UNSPECIFIED.);
#619=B_SPLINE_CURVE_WITH_KNOTS('',3,(#57070,#57071,#57072,#57073,#57074,
#57075,#57076,#57077,#57078,#57079),.UNSPECIFIED.,.F.,.F.,(4,1,1,1,1,1,
1,4),(15.7079632679489,16.6074319947502,17.6058755481493,18.6043191015485,
19.6027626549476,20.6012062083467,21.5996497617458,21.9911485751285),
 .UNSPECIFIED.);
#620=B_SPLINE_CURVE_WITH_KNOTS('',3,(#57080,#57081,#57082,#57083,#57084,
#57085,#57086,#57087,#57088,#57089),.UNSPECIFIED.,.F.,.F.,(4,1,1,1,1,1,
1,4),(15.7079632679489,16.3022811770509,17.30072473045,18.2991682838491,
19.2976118372482,20.2960553906474,21.2944989440465,21.9911485751285),
 .UNSPECIFIED.);
#621=B_SPLINE_CURVE_WITH_KNOTS('',3,(#57463,#57464,#57465,#57466,#57467,
#57468,#57469,#57470,#57471,#57472,#57473,#57474,#57475,#57476,#57477,#57478,
#57479,#57480,#57481,#57482,#57483,#57484,#57485,#57486,#57487,#57488,#57489,
#57490,#57491,#57492,#57493,#57494,#57495,#57496,#57497,#57498,#57499,#57500,
#57501,#57502,#57503,#57504,#57505,#57506,#57507,#57508,#57509,#57510,#57511,
#57512,#57513,#57514,#57515,#57516,#57517,#57518,#57519,#57520,#57521,#57522,
#57523,#57524,#57525,#57526,#57527,#57528,#57529),.UNSPECIFIED.,.F.,.F.,
(4,3,3,3,3,3,3,3,3,3,3,3,3,3,3,3,3,3,3,3,3,3,4),(0.,0.0253593625170432,
0.0904989134578323,0.129428846004824,0.149433065046328,0.165907354496605,
0.229382007773891,0.27252109928886,0.293394884079185,0.307837377566809,
0.368130738221205,0.401938373833768,0.435421038291672,0.450805053840956,
0.511072272729441,0.551886900769997,0.571326828937518,0.587500892696757,
0.626725156815222,0.649859628114584,0.67177310859451,0.727376664730075,
0.744397949170617),.UNSPECIFIED.);
#622=B_SPLINE_CURVE_WITH_KNOTS('',3,(#57530,#57531,#57532,#57533,#57534,
#57535,#57536,#57537,#57538,#57539,#57540,#57541,#57542,#57543,#57544,#57545,
#57546,#57547,#57548),.UNSPECIFIED.,.F.,.F.,(4,3,3,3,3,3,4),(82.7914542042459,
82.8708149321266,83.8692584855257,84.8677020389248,85.866145592324,86.8645891457231,
87.7987182084047),.UNSPECIFIED.);
#623=B_SPLINE_CURVE_WITH_KNOTS('',3,(#57550,#57551,#57552,#57553,#57554,
#57555,#57556,#57557,#57558,#57559,#57560,#57561,#57562,#57563,#57564,#57565,
#57566,#57567,#57568,#57569,#57570,#57571,#57572,#57573,#57574,#57575,#57576,
#57577,#57578,#57579,#57580,#57581,#57582,#57583,#57584,#57585,#57586,#57587,
#57588,#57589,#57590,#57591,#57592,#57593,#57594,#57595,#57596,#57597,#57598,
#57599,#57600,#57601,#57602,#57603,#57604,#57605,#57606,#57607,#57608,#57609,
#57610,#57611,#57612,#57613,#57614,#57615,#57616),.UNSPECIFIED.,.F.,.F.,
(4,3,3,3,3,3,3,3,3,3,3,3,3,3,3,3,3,3,3,3,3,3,4),(-0.744397949170599,-0.723387897941471,
-0.677960034185854,-0.66030178031912,-0.64147849017529,-0.603260261907819,
-0.580027150555408,-0.559762047797058,-0.499485193698097,-0.461022451958816,
-0.43985149859123,-0.426322963973344,-0.378677517214829,-0.331342827562976,
-0.308500355626486,-0.284779303920441,-0.222455882654308,-0.166841911990731,
-0.151140787742428,-0.135611969270085,-0.0678059846350425,-0.00370004143489645,
0.),.UNSPECIFIED.);
#624=B_SPLINE_CURVE_WITH_KNOTS('',3,(#57617,#57618,#57619,#57620,#57621,
#57622,#57623,#57624,#57625),.UNSPECIFIED.,.F.,.F.,(4,1,1,1,1,1,4),(10.3759343473737,
11.3100634100553,12.3085069634544,13.3069505168535,14.3053940702527,15.3038376236518,
15.7079632679489),.UNSPECIFIED.);
#625=B_SPLINE_CURVE_WITH_KNOTS('',3,(#57631,#57632,#57633,#57634,#57635,
#57636,#57637,#57638,#57639,#57640,#57641,#57642,#57643,#57644,#57645,#57646,
#57647,#57648,#57649,#57650,#57651,#57652,#57653,#57654,#57655,#57656,#57657,
#57658,#57659,#57660,#57661,#57662,#57663,#57664,#57665,#57666,#57667,#57668,
#57669,#57670,#57671,#57672,#57673,#57674,#57675,#57676,#57677,#57678,#57679,
#57680,#57681,#57682,#57683,#57684,#57685,#57686,#57687,#57688,#57689,#57690,
#57691),.UNSPECIFIED.,.F.,.F.,(4,3,3,3,3,3,3,3,3,3,3,3,3,3,3,3,3,3,3,3,
4),(-0.741270768406348,-0.716021136741387,-0.669194981720871,-0.640215156661528,
-0.6210285893087,-0.556595143115658,-0.539229517462428,-0.476555392316448,
-0.415575701759323,-0.398642849264355,-0.383309668681598,-0.34141189657726,
-0.279171652021188,-0.261540829450543,-0.245638028402519,-0.184228521301889,
-0.133954283551423,-0.117989348492863,-0.0589946742464315,-0.00428452387123181,
0.),.UNSPECIFIED.);
#626=B_SPLINE_CURVE_WITH_KNOTS('',3,(#57694,#57695,#57696,#57697,#57698,
#57699,#57700,#57701),.UNSPECIFIED.,.F.,.F.,(4,1,1,1,1,4),(11.6152142277547,
12.6136577811538,13.6121013345529,14.610544887952,15.6089884413511,15.7079632679489),
 .UNSPECIFIED.);
#627=B_SPLINE_CURVE_WITH_KNOTS('',3,(#58075,#58076,#58077,#58078,#58079,
#58080,#58081,#58082,#58083,#58084,#58085,#58086,#58087,#58088,#58089,#58090,
#58091,#58092,#58093,#58094,#58095,#58096,#58097,#58098,#58099,#58100,#58101,
#58102,#58103,#58104,#58105,#58106,#58107,#58108,#58109,#58110,#58111,#58112,
#58113,#58114,#58115,#58116,#58117,#58118,#58119,#58120,#58121,#58122,#58123,
#58124,#58125,#58126,#58127,#58128,#58129,#58130,#58131,#58132,#58133,#58134,
#58135,#58136,#58137,#58138),.UNSPECIFIED.,.F.,.F.,(4,3,3,3,3,3,3,3,3,3,
3,3,3,3,3,3,3,3,3,3,3,4),(0.,0.0209429534522624,0.0766684167144569,0.114857042461602,
0.130015240255125,0.189163540276417,0.2330164052432,0.259452045032286,0.274991797225966,
0.336182683058267,0.364575000143549,0.39776591033518,0.413108590858586,
0.474256684030488,0.514077927074317,0.537085464827502,0.55363870076605,
0.600546717676118,0.627087614796531,0.653616921528325,0.718721003615383,
0.741270768406323),.UNSPECIFIED.);
#628=B_SPLINE_CURVE_WITH_KNOTS('',3,(#58139,#58140,#58141,#58142,#58143,
#58144,#58145,#58146,#58147,#58148,#58149,#58150,#58151,#58152,#58153,#58154),
 .UNSPECIFIED.,.F.,.F.,(4,3,3,3,3,4),(-89.8599198059205,-88.8614762525213,
-87.8630326991222,-86.8645891457231,-85.866145592324,-85.7741580335289),
 .UNSPECIFIED.);
#1011=SHAPE_REPRESENTATION_RELATIONSHIP('SRR','None',#76748,#1031);
#1031=ADVANCED_BREP_SHAPE_REPRESENTATION('',(#1071),#76652);
#1051=STYLED_ITEM('',(#76913),#1071);
#1071=MANIFOLD_SOLID_BREP('Dog point set screw',#26676);
#1328=CYLINDRICAL_SURFACE('',#28290,0.3933);
#1329=CYLINDRICAL_SURFACE('',#28292,0.3933);
#1330=CYLINDRICAL_SURFACE('',#28293,0.3933);
#1331=CYLINDRICAL_SURFACE('',#28294,0.3933);
#1332=CYLINDRICAL_SURFACE('',#28295,0.3933);
#1333=CYLINDRICAL_SURFACE('',#28296,0.3933);
#1334=CYLINDRICAL_SURFACE('',#28297,0.3933);
#1335=CYLINDRICAL_SURFACE('',#28298,0.3933);
#1336=CYLINDRICAL_SURFACE('',#28299,0.3933);
#1337=CYLINDRICAL_SURFACE('',#28300,0.3933);
#1338=CYLINDRICAL_SURFACE('',#28301,0.3933);
#1339=CYLINDRICAL_SURFACE('',#28302,0.3933);
#1340=CYLINDRICAL_SURFACE('',#28303,0.3933);
#1341=CYLINDRICAL_SURFACE('',#28304,0.3933);
#1342=CYLINDRICAL_SURFACE('',#28305,0.322275);
#1343=CYLINDRICAL_SURFACE('',#28307,0.322275);
#1344=CYLINDRICAL_SURFACE('',#28308,0.322275);
#1345=CYLINDRICAL_SURFACE('',#28309,0.322275);
#1346=CYLINDRICAL_SURFACE('',#28310,0.322275);
#1347=CYLINDRICAL_SURFACE('',#28311,0.322275);
#1348=CYLINDRICAL_SURFACE('',#28312,0.322275);
#1349=CYLINDRICAL_SURFACE('',#28313,0.322275);
#1350=CYLINDRICAL_SURFACE('',#28314,0.322275);
#1351=CYLINDRICAL_SURFACE('',#28315,0.322275);
#1352=CYLINDRICAL_SURFACE('',#28316,0.322275);
#1353=CYLINDRICAL_SURFACE('',#28317,0.322275);
#1354=CYLINDRICAL_SURFACE('',#28318,0.322275);
#1355=CYLINDRICAL_SURFACE('',#28319,0.322275);
#1356=CYLINDRICAL_SURFACE('',#28324,0.322275);
#1357=CYLINDRICAL_SURFACE('',#28338,0.3933);
#1358=CYLINDRICAL_SURFACE('',#28339,0.275);
#1638=FACE_BOUND('',#5060,.T.);
#1639=FACE_BOUND('',#5069,.T.);
#2119=PLANE('',#28320);
#2120=PLANE('',#28325);
#2121=PLANE('',#28328);
#2122=PLANE('',#28329);
#2123=PLANE('',#28330);
#2124=PLANE('',#28331);
#2125=PLANE('',#28332);
#2126=PLANE('',#28333);
#2127=PLANE('',#28334);
#2128=PLANE('',#28335);
#2129=PLANE('',#28343);
#3390=FACE_OUTER_BOUND('',#5027,.T.);
#3391=FACE_OUTER_BOUND('',#5028,.T.);
#3392=FACE_OUTER_BOUND('',#5029,.T.);
#3393=FACE_OUTER_BOUND('',#5030,.T.);
#3394=FACE_OUTER_BOUND('',#5031,.T.);
#3395=FACE_OUTER_BOUND('',#5032,.T.);
#3396=FACE_OUTER_BOUND('',#5033,.T.);
#3397=FACE_OUTER_BOUND('',#5034,.T.);
#3398=FACE_OUTER_BOUND('',#5035,.T.);
#3399=FACE_OUTER_BOUND('',#5036,.T.);
#3400=FACE_OUTER_BOUND('',#5037,.T.);
#3401=FACE_OUTER_BOUND('',#5038,.T.);
#3402=FACE_OUTER_BOUND('',#5039,.T.);
#3403=FACE_OUTER_BOUND('',#5040,.T.);
#3404=FACE_OUTER_BOUND('',#5041,.T.);
#3405=FACE_OUTER_BOUND('',#5042,.T.);
#3406=FACE_OUTER_BOUND('',#5043,.T.);
#3407=FACE_OUTER_BOUND('',#5044,.T.);
#3408=FACE_OUTER_BOUND('',#5045,.T.);
#3409=FACE_OUTER_BOUND('',#5046,.T.);
#3410=FACE_OUTER_BOUND('',#5047,.T.);
#3411=FACE_OUTER_BOUND('',#5048,.T.);
#3412=FACE_OUTER_BOUND('',#5049,.T.);
#3413=FACE_OUTER_BOUND('',#5050,.T.);
#3414=FACE_OUTER_BOUND('',#5051,.T.);
#3415=FACE_OUTER_BOUND('',#5052,.T.);
#3416=FACE_OUTER_BOUND('',#5053,.T.);
#3417=FACE_OUTER_BOUND('',#5054,.T.);
#3418=FACE_OUTER_BOUND('',#5055,.T.);
#3419=FACE_OUTER_BOUND('',#5056,.T.);
#3420=FACE_OUTER_BOUND('',#5057,.T.);
#3421=FACE_OUTER_BOUND('',#5058,.T.);
#3422=FACE_OUTER_BOUND('',#5059,.T.);
#3423=FACE_OUTER_BOUND('',#5061,.T.);
#3424=FACE_OUTER_BOUND('',#5062,.T.);
#3425=FACE_OUTER_BOUND('',#5063,.T.);
#3426=FACE_OUTER_BOUND('',#5064,.T.);
#3427=FACE_OUTER_BOUND('',#5065,.T.);
#3428=FACE_OUTER_BOUND('',#5066,.T.);
#3429=FACE_OUTER_BOUND('',#5067,.T.);
#3430=FACE_OUTER_BOUND('',#5068,.T.);
#3431=FACE_OUTER_BOUND('',#5070,.T.);
#3432=FACE_OUTER_BOUND('',#5071,.T.);
#3433=FACE_OUTER_BOUND('',#5072,.T.);
#3434=FACE_OUTER_BOUND('',#5073,.T.);
#3435=FACE_OUTER_BOUND('',#5074,.T.);
#5027=EDGE_LOOP('',(#21459,#21460,#21461,#21462));
#5028=EDGE_LOOP('',(#21463,#21464,#21465,#21466));
#5029=EDGE_LOOP('',(#21467,#21468,#21469,#21470));
#5030=EDGE_LOOP('',(#21471,#21472,#21473,#21474));
#5031=EDGE_LOOP('',(#21475,#21476,#21477,#21478));
#5032=EDGE_LOOP('',(#21479,#21480,#21481,#21482));
#5033=EDGE_LOOP('',(#21483,#21484,#21485,#21486));
#5034=EDGE_LOOP('',(#21487,#21488,#21489,#21490));
#5035=EDGE_LOOP('',(#21491,#21492,#21493,#21494));
#5036=EDGE_LOOP('',(#21495,#21496,#21497,#21498));
#5037=EDGE_LOOP('',(#21499,#21500,#21501,#21502));
#5038=EDGE_LOOP('',(#21503,#21504,#21505,#21506));
#5039=EDGE_LOOP('',(#21507,#21508,#21509,#21510));
#5040=EDGE_LOOP('',(#21511,#21512,#21513,#21514));
#5041=EDGE_LOOP('',(#21515,#21516,#21517,#21518));
#5042=EDGE_LOOP('',(#21519,#21520,#21521,#21522));
#5043=EDGE_LOOP('',(#21523,#21524,#21525,#21526));
#5044=EDGE_LOOP('',(#21527,#21528,#21529,#21530));
#5045=EDGE_LOOP('',(#21531,#21532,#21533,#21534));
#5046=EDGE_LOOP('',(#21535,#21536,#21537,#21538));
#5047=EDGE_LOOP('',(#21539,#21540,#21541,#21542));
#5048=EDGE_LOOP('',(#21543,#21544,#21545,#21546));
#5049=EDGE_LOOP('',(#21547,#21548,#21549,#21550));
#5050=EDGE_LOOP('',(#21551,#21552,#21553,#21554));
#5051=EDGE_LOOP('',(#21555,#21556,#21557,#21558));
#5052=EDGE_LOOP('',(#21559,#21560,#21561,#21562));
#5053=EDGE_LOOP('',(#21563,#21564,#21565,#21566));
#5054=EDGE_LOOP('',(#21567,#21568,#21569,#21570));
#5055=EDGE_LOOP('',(#21571,#21572,#21573,#21574,#21575,#21576,#21577,#21578,
#21579,#21580,#21581,#21582,#21583,#21584,#21585,#21586,#21587,#21588,#21589,
#21590,#21591,#21592,#21593,#21594,#21595,#21596,#21597,#21598,#21599,#21600,
#21601,#21602));
#5056=EDGE_LOOP('',(#21603,#21604,#21605,#21606,#21607));
#5057=EDGE_LOOP('',(#21608,#21609,#21610,#21611));
#5058=EDGE_LOOP('',(#21612,#21613,#21614,#21615,#21616,#21617,#21618,#21619,
#21620,#21621,#21622,#21623,#21624,#21625,#21626,#21627,#21628,#21629,#21630,
#21631,#21632,#21633,#21634,#21635,#21636,#21637,#21638,#21639,#21640,#21641,
#21642,#21643));
#5059=EDGE_LOOP('',(#21644,#21645,#21646,#21647));
#5060=EDGE_LOOP('',(#21648));
#5061=EDGE_LOOP('',(#21649,#21650,#21651,#21652));
#5062=EDGE_LOOP('',(#21653,#21654,#21655,#21656));
#5063=EDGE_LOOP('',(#21657,#21658,#21659,#21660));
#5064=EDGE_LOOP('',(#21661,#21662,#21663,#21664));
#5065=EDGE_LOOP('',(#21665,#21666,#21667,#21668));
#5066=EDGE_LOOP('',(#21669,#21670,#21671,#21672));
#5067=EDGE_LOOP('',(#21673,#21674,#21675,#21676,#21677,#21678));
#5068=EDGE_LOOP('',(#21679));
#5069=EDGE_LOOP('',(#21680,#21681,#21682,#21683,#21684,#21685));
#5070=EDGE_LOOP('',(#21686,#21687,#21688,#21689,#21690,#21691));
#5071=EDGE_LOOP('',(#21692,#21693,#21694,#21695));
#5072=EDGE_LOOP('',(#21696,#21697,#21698,#21699));
#5073=EDGE_LOOP('',(#21700,#21701,#21702,#21703));
#5074=EDGE_LOOP('',(#21704));
#6248=CIRCLE('',#28291,0.3933);
#6249=CIRCLE('',#28306,0.322275);
#6250=CIRCLE('',#28321,0.3933);
#6251=CIRCLE('',#28322,0.3933);
#6252=CIRCLE('',#28323,0.322275);
#6253=CIRCLE('',#28326,0.3933);
#6254=CIRCLE('',#28327,0.275);
#6255=CIRCLE('',#28336,0.34);
#6256=CIRCLE('',#28340,0.275);
#6257=CIRCLE('',#28342,0.245);
#7807=LINE('',#56091,#9963);
#7808=LINE('',#56115,#9964);
#7809=LINE('',#56163,#9965);
#7810=LINE('',#56211,#9966);
#7811=LINE('',#56259,#9967);
#7812=LINE('',#56313,#9968);
#7813=LINE('',#56361,#9969);
#7814=LINE('',#56409,#9970);
#7815=LINE('',#56463,#9971);
#7816=LINE('',#56511,#9972);
#7817=LINE('',#56559,#9973);
#7818=LINE('',#56613,#9974);
#7819=LINE('',#56661,#9975);
#7820=LINE('',#56709,#9976);
#7821=LINE('',#56757,#9977);
#7822=LINE('',#56774,#9978);
#7823=LINE('',#56799,#9979);
#7824=LINE('',#56823,#9980);
#7825=LINE('',#56847,#9981);
#7826=LINE('',#56872,#9982);
#7827=LINE('',#56897,#9983);
#7828=LINE('',#56921,#9984);
#7829=LINE('',#56946,#9985);
#7830=LINE('',#56971,#9986);
#7831=LINE('',#56995,#9987);
#7832=LINE('',#57020,#9988);
#7833=LINE('',#57045,#9989);
#7834=LINE('',#57069,#9990);
#7835=LINE('',#58162,#9991);
#7836=LINE('',#58164,#9992);
#7837=LINE('',#58166,#9993);
#7838=LINE('',#58167,#9994);
#7839=LINE('',#58170,#9995);
#7840=LINE('',#58172,#9996);
#7841=LINE('',#58173,#9997);
#7842=LINE('',#58176,#9998);
#7843=LINE('',#58178,#9999);
#7844=LINE('',#58179,#10000);
#7845=LINE('',#58182,#10001);
#7846=LINE('',#58184,#10002);
#7847=LINE('',#58185,#10003);
#7848=LINE('',#58188,#10004);
#7849=LINE('',#58190,#10005);
#7850=LINE('',#58191,#10006);
#7851=LINE('',#58193,#10007);
#7852=LINE('',#58194,#10008);
#7853=LINE('',#58200,#10009);
#7854=LINE('',#58205,#10010);
#7855=LINE('',#58209,#10011);
#9963=VECTOR('',#33332,0.4);
#9964=VECTOR('',#33337,0.4);
#9965=VECTOR('',#33340,0.4);
#9966=VECTOR('',#33343,0.4);
#9967=VECTOR('',#33346,0.4);
#9968=VECTOR('',#33349,0.4);
#9969=VECTOR('',#33352,0.4);
#9970=VECTOR('',#33355,0.4);
#9971=VECTOR('',#33358,0.4);
#9972=VECTOR('',#33361,0.4);
#9973=VECTOR('',#33364,0.4);
#9974=VECTOR('',#33367,0.4);
#9975=VECTOR('',#33370,0.4);
#9976=VECTOR('',#33373,0.4);
#9977=VECTOR('',#33376,0.322275);
#9978=VECTOR('',#33381,0.322275);
#9979=VECTOR('',#33384,0.322275);
#9980=VECTOR('',#33387,0.322275);
#9981=VECTOR('',#33390,0.322275);
#9982=VECTOR('',#33393,0.322275);
#9983=VECTOR('',#33396,0.322275);
#9984=VECTOR('',#33399,0.322275);
#9985=VECTOR('',#33402,0.322275);
#9986=VECTOR('',#33405,0.322275);
#9987=VECTOR('',#33408,0.322275);
#9988=VECTOR('',#33411,0.322275);
#9989=VECTOR('',#33414,0.322275);
#9990=VECTOR('',#33417,0.322275);
#9991=VECTOR('',#33436,1.);
#9992=VECTOR('',#33437,1.);
#9993=VECTOR('',#33438,1.);
#9994=VECTOR('',#33439,1.);
#9995=VECTOR('',#33442,1.);
#9996=VECTOR('',#33443,1.);
#9997=VECTOR('',#33444,1.);
#9998=VECTOR('',#33447,1.);
#9999=VECTOR('',#33448,1.);
#10000=VECTOR('',#33449,1.);
#10001=VECTOR('',#33452,1.);
#10002=VECTOR('',#33453,1.);
#10003=VECTOR('',#33454,1.);
#10004=VECTOR('',#33457,1.);
#10005=VECTOR('',#33458,1.);
#10006=VECTOR('',#33459,1.);
#10007=VECTOR('',#33462,1.);
#10008=VECTOR('',#33463,1.);
#10009=VECTOR('',#33472,0.37);
#10010=VECTOR('',#33479,0.275);
#10011=VECTOR('',#33484,0.26);
#12238=VERTEX_POINT('',#56089);
#12239=VERTEX_POINT('',#56090);
#12240=VERTEX_POINT('',#56092);
#12241=VERTEX_POINT('',#56103);
#12242=VERTEX_POINT('',#56113);
#12243=VERTEX_POINT('',#56114);
#12244=VERTEX_POINT('',#56161);
#12245=VERTEX_POINT('',#56162);
#12246=VERTEX_POINT('',#56209);
#12247=VERTEX_POINT('',#56210);
#12248=VERTEX_POINT('',#56257);
#12249=VERTEX_POINT('',#56258);
#12250=VERTEX_POINT('',#56311);
#12251=VERTEX_POINT('',#56312);
#12252=VERTEX_POINT('',#56359);
#12253=VERTEX_POINT('',#56360);
#12254=VERTEX_POINT('',#56407);
#12255=VERTEX_POINT('',#56408);
#12256=VERTEX_POINT('',#56461);
#12257=VERTEX_POINT('',#56462);
#12258=VERTEX_POINT('',#56509);
#12259=VERTEX_POINT('',#56510);
#12260=VERTEX_POINT('',#56557);
#12261=VERTEX_POINT('',#56558);
#12262=VERTEX_POINT('',#56611);
#12263=VERTEX_POINT('',#56612);
#12264=VERTEX_POINT('',#56659);
#12265=VERTEX_POINT('',#56660);
#12266=VERTEX_POINT('',#56707);
#12267=VERTEX_POINT('',#56708);
#12268=VERTEX_POINT('',#56755);
#12269=VERTEX_POINT('',#56756);
#12270=VERTEX_POINT('',#56758);
#12271=VERTEX_POINT('',#56765);
#12272=VERTEX_POINT('',#56772);
#12273=VERTEX_POINT('',#56773);
#12274=VERTEX_POINT('',#56797);
#12275=VERTEX_POINT('',#56798);
#12276=VERTEX_POINT('',#56821);
#12277=VERTEX_POINT('',#56822);
#12278=VERTEX_POINT('',#56845);
#12279=VERTEX_POINT('',#56846);
#12280=VERTEX_POINT('',#56870);
#12281=VERTEX_POINT('',#56871);
#12282=VERTEX_POINT('',#56895);
#12283=VERTEX_POINT('',#56896);
#12284=VERTEX_POINT('',#56919);
#12285=VERTEX_POINT('',#56920);
#12286=VERTEX_POINT('',#56944);
#12287=VERTEX_POINT('',#56945);
#12288=VERTEX_POINT('',#56969);
#12289=VERTEX_POINT('',#56970);
#12290=VERTEX_POINT('',#56993);
#12291=VERTEX_POINT('',#56994);
#12292=VERTEX_POINT('',#57018);
#12293=VERTEX_POINT('',#57019);
#12294=VERTEX_POINT('',#57043);
#12295=VERTEX_POINT('',#57044);
#12296=VERTEX_POINT('',#57067);
#12297=VERTEX_POINT('',#57068);
#12298=VERTEX_POINT('',#57462);
#12299=VERTEX_POINT('',#57549);
#12300=VERTEX_POINT('',#57627);
#12301=VERTEX_POINT('',#57630);
#12302=VERTEX_POINT('',#58074);
#12303=VERTEX_POINT('',#58157);
#12304=VERTEX_POINT('',#58160);
#12305=VERTEX_POINT('',#58161);
#12306=VERTEX_POINT('',#58163);
#12307=VERTEX_POINT('',#58165);
#12308=VERTEX_POINT('',#58169);
#12309=VERTEX_POINT('',#58171);
#12310=VERTEX_POINT('',#58175);
#12311=VERTEX_POINT('',#58177);
#12312=VERTEX_POINT('',#58181);
#12313=VERTEX_POINT('',#58183);
#12314=VERTEX_POINT('',#58187);
#12315=VERTEX_POINT('',#58189);
#12316=VERTEX_POINT('',#58197);
#12317=VERTEX_POINT('',#58203);
#12318=VERTEX_POINT('',#58207);
#15452=EDGE_CURVE('',#12238,#12239,#7807,.T.);
#15453=EDGE_CURVE('',#12238,#12240,#565,.T.);
#15454=EDGE_CURVE('',#12240,#12241,#6248,.T.);
#15455=EDGE_CURVE('',#12241,#12239,#566,.T.);
#15456=EDGE_CURVE('',#12242,#12243,#7808,.T.);
#15457=EDGE_CURVE('',#12242,#12238,#567,.T.);
#15458=EDGE_CURVE('',#12239,#12243,#568,.T.);
#15459=EDGE_CURVE('',#12244,#12245,#7809,.T.);
#15460=EDGE_CURVE('',#12244,#12242,#569,.T.);
#15461=EDGE_CURVE('',#12243,#12245,#570,.T.);
#15462=EDGE_CURVE('',#12246,#12247,#7810,.T.);
#15463=EDGE_CURVE('',#12246,#12244,#571,.T.);
#15464=EDGE_CURVE('',#12245,#12247,#572,.T.);
#15465=EDGE_CURVE('',#12248,#12249,#7811,.T.);
#15466=EDGE_CURVE('',#12248,#12246,#573,.T.);
#15467=EDGE_CURVE('',#12247,#12249,#574,.T.);
#15468=EDGE_CURVE('',#12250,#12251,#7812,.T.);
#15469=EDGE_CURVE('',#12250,#12248,#575,.T.);
#15470=EDGE_CURVE('',#12249,#12251,#576,.T.);
#15471=EDGE_CURVE('',#12252,#12253,#7813,.T.);
#15472=EDGE_CURVE('',#12252,#12250,#577,.T.);
#15473=EDGE_CURVE('',#12251,#12253,#578,.T.);
#15474=EDGE_CURVE('',#12254,#12255,#7814,.T.);
#15475=EDGE_CURVE('',#12254,#12252,#579,.T.);
#15476=EDGE_CURVE('',#12253,#12255,#580,.T.);
#15477=EDGE_CURVE('',#12256,#12257,#7815,.T.);
#15478=EDGE_CURVE('',#12256,#12254,#581,.T.);
#15479=EDGE_CURVE('',#12255,#12257,#582,.T.);
#15480=EDGE_CURVE('',#12258,#12259,#7816,.T.);
#15481=EDGE_CURVE('',#12258,#12256,#583,.T.);
#15482=EDGE_CURVE('',#12257,#12259,#584,.T.);
#15483=EDGE_CURVE('',#12260,#12261,#7817,.T.);
#15484=EDGE_CURVE('',#12260,#12258,#585,.T.);
#15485=EDGE_CURVE('',#12259,#12261,#586,.T.);
#15486=EDGE_CURVE('',#12262,#12263,#7818,.T.);
#15487=EDGE_CURVE('',#12262,#12260,#587,.T.);
#15488=EDGE_CURVE('',#12261,#12263,#588,.T.);
#15489=EDGE_CURVE('',#12264,#12265,#7819,.T.);
#15490=EDGE_CURVE('',#12264,#12262,#589,.T.);
#15491=EDGE_CURVE('',#12263,#12265,#590,.T.);
#15492=EDGE_CURVE('',#12266,#12267,#7820,.T.);
#15493=EDGE_CURVE('',#12266,#12264,#591,.T.);
#15494=EDGE_CURVE('',#12265,#12267,#592,.T.);
#15495=EDGE_CURVE('',#12268,#12269,#7821,.T.);
#15496=EDGE_CURVE('',#12268,#12270,#593,.T.);
#15497=EDGE_CURVE('',#12271,#12270,#6249,.T.);
#15498=EDGE_CURVE('',#12269,#12271,#594,.T.);
#15499=EDGE_CURVE('',#12272,#12273,#7822,.T.);
#15500=EDGE_CURVE('',#12272,#12268,#595,.T.);
#15501=EDGE_CURVE('',#12273,#12269,#596,.T.);
#15502=EDGE_CURVE('',#12274,#12275,#7823,.T.);
#15503=EDGE_CURVE('',#12274,#12272,#597,.T.);
#15504=EDGE_CURVE('',#12275,#12273,#598,.T.);
#15505=EDGE_CURVE('',#12276,#12277,#7824,.T.);
#15506=EDGE_CURVE('',#12276,#12274,#599,.T.);
#15507=EDGE_CURVE('',#12277,#12275,#600,.T.);
#15508=EDGE_CURVE('',#12278,#12279,#7825,.T.);
#15509=EDGE_CURVE('',#12278,#12276,#601,.T.);
#15510=EDGE_CURVE('',#12279,#12277,#602,.T.);
#15511=EDGE_CURVE('',#12280,#12281,#7826,.T.);
#15512=EDGE_CURVE('',#12280,#12278,#603,.T.);
#15513=EDGE_CURVE('',#12281,#12279,#604,.T.);
#15514=EDGE_CURVE('',#12282,#12283,#7827,.T.);
#15515=EDGE_CURVE('',#12282,#12280,#605,.T.);
#15516=EDGE_CURVE('',#12283,#12281,#606,.T.);
#15517=EDGE_CURVE('',#12284,#12285,#7828,.T.);
#15518=EDGE_CURVE('',#12284,#12282,#607,.T.);
#15519=EDGE_CURVE('',#12285,#12283,#608,.T.);
#15520=EDGE_CURVE('',#12286,#12287,#7829,.T.);
#15521=EDGE_CURVE('',#12286,#12284,#609,.T.);
#15522=EDGE_CURVE('',#12287,#12285,#610,.T.);
#15523=EDGE_CURVE('',#12288,#12289,#7830,.T.);
#15524=EDGE_CURVE('',#12288,#12286,#611,.T.);
#15525=EDGE_CURVE('',#12289,#12287,#612,.T.);
#15526=EDGE_CURVE('',#12290,#12291,#7831,.T.);
#15527=EDGE_CURVE('',#12290,#12288,#613,.T.);
#15528=EDGE_CURVE('',#12291,#12289,#614,.T.);
#15529=EDGE_CURVE('',#12292,#12293,#7832,.T.);
#15530=EDGE_CURVE('',#12292,#12290,#615,.T.);
#15531=EDGE_CURVE('',#12293,#12291,#616,.T.);
#15532=EDGE_CURVE('',#12294,#12295,#7833,.T.);
#15533=EDGE_CURVE('',#12294,#12292,#617,.T.);
#15534=EDGE_CURVE('',#12295,#12293,#618,.T.);
#15535=EDGE_CURVE('',#12296,#12297,#7834,.T.);
#15536=EDGE_CURVE('',#12296,#12294,#619,.T.);
#15537=EDGE_CURVE('',#12297,#12295,#620,.T.);
#15538=EDGE_CURVE('',#12298,#12271,#621,.T.);
#15539=EDGE_CURVE('',#12267,#12298,#622,.T.);
#15540=EDGE_CURVE('',#12299,#12241,#623,.T.);
#15541=EDGE_CURVE('',#12299,#12297,#624,.T.);
#15542=EDGE_CURVE('',#12241,#12300,#6250,.T.);
#15543=EDGE_CURVE('',#12300,#12240,#6251,.T.);
#15544=EDGE_CURVE('',#12240,#12301,#625,.T.);
#15545=EDGE_CURVE('',#12301,#12299,#6252,.T.);
#15546=EDGE_CURVE('',#12301,#12296,#626,.T.);
#15547=EDGE_CURVE('',#12270,#12302,#627,.T.);
#15548=EDGE_CURVE('',#12302,#12266,#628,.T.);
#15549=EDGE_CURVE('',#12302,#12298,#6253,.F.);
#15550=EDGE_CURVE('',#12303,#12303,#6254,.T.);
#15551=EDGE_CURVE('',#12304,#12305,#7835,.T.);
#15552=EDGE_CURVE('',#12304,#12306,#7836,.T.);
#15553=EDGE_CURVE('',#12306,#12307,#7837,.T.);
#15554=EDGE_CURVE('',#12305,#12307,#7838,.T.);
#15555=EDGE_CURVE('',#12308,#12304,#7839,.T.);
#15556=EDGE_CURVE('',#12308,#12309,#7840,.T.);
#15557=EDGE_CURVE('',#12309,#12306,#7841,.T.);
#15558=EDGE_CURVE('',#12310,#12308,#7842,.T.);
#15559=EDGE_CURVE('',#12310,#12311,#7843,.T.);
#15560=EDGE_CURVE('',#12311,#12309,#7844,.T.);
#15561=EDGE_CURVE('',#12312,#12310,#7845,.T.);
#15562=EDGE_CURVE('',#12312,#12313,#7846,.T.);
#15563=EDGE_CURVE('',#12313,#12311,#7847,.T.);
#15564=EDGE_CURVE('',#12314,#12312,#7848,.T.);
#15565=EDGE_CURVE('',#12314,#12315,#7849,.T.);
#15566=EDGE_CURVE('',#12315,#12313,#7850,.T.);
#15567=EDGE_CURVE('',#12305,#12314,#7851,.T.);
#15568=EDGE_CURVE('',#12307,#12315,#7852,.T.);
#15569=EDGE_CURVE('',#12316,#12316,#6255,.T.);
#15570=EDGE_CURVE('',#12300,#12316,#7853,.T.);
#15571=EDGE_CURVE('',#12317,#12317,#6256,.T.);
#15572=EDGE_CURVE('',#12317,#12303,#7854,.T.);
#15573=EDGE_CURVE('',#12318,#12318,#6257,.T.);
#15574=EDGE_CURVE('',#12318,#12317,#7855,.T.);
#21459=ORIENTED_EDGE('',*,*,#15452,.F.);
#21460=ORIENTED_EDGE('',*,*,#15453,.T.);
#21461=ORIENTED_EDGE('',*,*,#15454,.T.);
#21462=ORIENTED_EDGE('',*,*,#15455,.T.);
#21463=ORIENTED_EDGE('',*,*,#15456,.F.);
#21464=ORIENTED_EDGE('',*,*,#15457,.T.);
#21465=ORIENTED_EDGE('',*,*,#15452,.T.);
#21466=ORIENTED_EDGE('',*,*,#15458,.T.);
#21467=ORIENTED_EDGE('',*,*,#15459,.F.);
#21468=ORIENTED_EDGE('',*,*,#15460,.T.);
#21469=ORIENTED_EDGE('',*,*,#15456,.T.);
#21470=ORIENTED_EDGE('',*,*,#15461,.T.);
#21471=ORIENTED_EDGE('',*,*,#15462,.F.);
#21472=ORIENTED_EDGE('',*,*,#15463,.T.);
#21473=ORIENTED_EDGE('',*,*,#15459,.T.);
#21474=ORIENTED_EDGE('',*,*,#15464,.T.);
#21475=ORIENTED_EDGE('',*,*,#15465,.F.);
#21476=ORIENTED_EDGE('',*,*,#15466,.T.);
#21477=ORIENTED_EDGE('',*,*,#15462,.T.);
#21478=ORIENTED_EDGE('',*,*,#15467,.T.);
#21479=ORIENTED_EDGE('',*,*,#15468,.F.);
#21480=ORIENTED_EDGE('',*,*,#15469,.T.);
#21481=ORIENTED_EDGE('',*,*,#15465,.T.);
#21482=ORIENTED_EDGE('',*,*,#15470,.T.);
#21483=ORIENTED_EDGE('',*,*,#15471,.F.);
#21484=ORIENTED_EDGE('',*,*,#15472,.T.);
#21485=ORIENTED_EDGE('',*,*,#15468,.T.);
#21486=ORIENTED_EDGE('',*,*,#15473,.T.);
#21487=ORIENTED_EDGE('',*,*,#15474,.F.);
#21488=ORIENTED_EDGE('',*,*,#15475,.T.);
#21489=ORIENTED_EDGE('',*,*,#15471,.T.);
#21490=ORIENTED_EDGE('',*,*,#15476,.T.);
#21491=ORIENTED_EDGE('',*,*,#15477,.F.);
#21492=ORIENTED_EDGE('',*,*,#15478,.T.);
#21493=ORIENTED_EDGE('',*,*,#15474,.T.);
#21494=ORIENTED_EDGE('',*,*,#15479,.T.);
#21495=ORIENTED_EDGE('',*,*,#15480,.F.);
#21496=ORIENTED_EDGE('',*,*,#15481,.T.);
#21497=ORIENTED_EDGE('',*,*,#15477,.T.);
#21498=ORIENTED_EDGE('',*,*,#15482,.T.);
#21499=ORIENTED_EDGE('',*,*,#15483,.F.);
#21500=ORIENTED_EDGE('',*,*,#15484,.T.);
#21501=ORIENTED_EDGE('',*,*,#15480,.T.);
#21502=ORIENTED_EDGE('',*,*,#15485,.T.);
#21503=ORIENTED_EDGE('',*,*,#15486,.F.);
#21504=ORIENTED_EDGE('',*,*,#15487,.T.);
#21505=ORIENTED_EDGE('',*,*,#15483,.T.);
#21506=ORIENTED_EDGE('',*,*,#15488,.T.);
#21507=ORIENTED_EDGE('',*,*,#15489,.F.);
#21508=ORIENTED_EDGE('',*,*,#15490,.T.);
#21509=ORIENTED_EDGE('',*,*,#15486,.T.);
#21510=ORIENTED_EDGE('',*,*,#15491,.T.);
#21511=ORIENTED_EDGE('',*,*,#15492,.F.);
#21512=ORIENTED_EDGE('',*,*,#15493,.T.);
#21513=ORIENTED_EDGE('',*,*,#15489,.T.);
#21514=ORIENTED_EDGE('',*,*,#15494,.T.);
#21515=ORIENTED_EDGE('',*,*,#15495,.F.);
#21516=ORIENTED_EDGE('',*,*,#15496,.T.);
#21517=ORIENTED_EDGE('',*,*,#15497,.F.);
#21518=ORIENTED_EDGE('',*,*,#15498,.F.);
#21519=ORIENTED_EDGE('',*,*,#15499,.F.);
#21520=ORIENTED_EDGE('',*,*,#15500,.T.);
#21521=ORIENTED_EDGE('',*,*,#15495,.T.);
#21522=ORIENTED_EDGE('',*,*,#15501,.F.);
#21523=ORIENTED_EDGE('',*,*,#15502,.F.);
#21524=ORIENTED_EDGE('',*,*,#15503,.T.);
#21525=ORIENTED_EDGE('',*,*,#15499,.T.);
#21526=ORIENTED_EDGE('',*,*,#15504,.F.);
#21527=ORIENTED_EDGE('',*,*,#15505,.F.);
#21528=ORIENTED_EDGE('',*,*,#15506,.T.);
#21529=ORIENTED_EDGE('',*,*,#15502,.T.);
#21530=ORIENTED_EDGE('',*,*,#15507,.F.);
#21531=ORIENTED_EDGE('',*,*,#15508,.F.);
#21532=ORIENTED_EDGE('',*,*,#15509,.T.);
#21533=ORIENTED_EDGE('',*,*,#15505,.T.);
#21534=ORIENTED_EDGE('',*,*,#15510,.F.);
#21535=ORIENTED_EDGE('',*,*,#15511,.F.);
#21536=ORIENTED_EDGE('',*,*,#15512,.T.);
#21537=ORIENTED_EDGE('',*,*,#15508,.T.);
#21538=ORIENTED_EDGE('',*,*,#15513,.F.);
#21539=ORIENTED_EDGE('',*,*,#15514,.F.);
#21540=ORIENTED_EDGE('',*,*,#15515,.T.);
#21541=ORIENTED_EDGE('',*,*,#15511,.T.);
#21542=ORIENTED_EDGE('',*,*,#15516,.F.);
#21543=ORIENTED_EDGE('',*,*,#15517,.F.);
#21544=ORIENTED_EDGE('',*,*,#15518,.T.);
#21545=ORIENTED_EDGE('',*,*,#15514,.T.);
#21546=ORIENTED_EDGE('',*,*,#15519,.F.);
#21547=ORIENTED_EDGE('',*,*,#15520,.F.);
#21548=ORIENTED_EDGE('',*,*,#15521,.T.);
#21549=ORIENTED_EDGE('',*,*,#15517,.T.);
#21550=ORIENTED_EDGE('',*,*,#15522,.F.);
#21551=ORIENTED_EDGE('',*,*,#15523,.F.);
#21552=ORIENTED_EDGE('',*,*,#15524,.T.);
#21553=ORIENTED_EDGE('',*,*,#15520,.T.);
#21554=ORIENTED_EDGE('',*,*,#15525,.F.);
#21555=ORIENTED_EDGE('',*,*,#15526,.F.);
#21556=ORIENTED_EDGE('',*,*,#15527,.T.);
#21557=ORIENTED_EDGE('',*,*,#15523,.T.);
#21558=ORIENTED_EDGE('',*,*,#15528,.F.);
#21559=ORIENTED_EDGE('',*,*,#15529,.F.);
#21560=ORIENTED_EDGE('',*,*,#15530,.T.);
#21561=ORIENTED_EDGE('',*,*,#15526,.T.);
#21562=ORIENTED_EDGE('',*,*,#15531,.F.);
#21563=ORIENTED_EDGE('',*,*,#15532,.F.);
#21564=ORIENTED_EDGE('',*,*,#15533,.T.);
#21565=ORIENTED_EDGE('',*,*,#15529,.T.);
#21566=ORIENTED_EDGE('',*,*,#15534,.F.);
#21567=ORIENTED_EDGE('',*,*,#15535,.F.);
#21568=ORIENTED_EDGE('',*,*,#15536,.T.);
#21569=ORIENTED_EDGE('',*,*,#15532,.T.);
#21570=ORIENTED_EDGE('',*,*,#15537,.F.);
#21571=ORIENTED_EDGE('',*,*,#15538,.F.);
#21572=ORIENTED_EDGE('',*,*,#15539,.F.);
#21573=ORIENTED_EDGE('',*,*,#15494,.F.);
#21574=ORIENTED_EDGE('',*,*,#15491,.F.);
#21575=ORIENTED_EDGE('',*,*,#15488,.F.);
#21576=ORIENTED_EDGE('',*,*,#15485,.F.);
#21577=ORIENTED_EDGE('',*,*,#15482,.F.);
#21578=ORIENTED_EDGE('',*,*,#15479,.F.);
#21579=ORIENTED_EDGE('',*,*,#15476,.F.);
#21580=ORIENTED_EDGE('',*,*,#15473,.F.);
#21581=ORIENTED_EDGE('',*,*,#15470,.F.);
#21582=ORIENTED_EDGE('',*,*,#15467,.F.);
#21583=ORIENTED_EDGE('',*,*,#15464,.F.);
#21584=ORIENTED_EDGE('',*,*,#15461,.F.);
#21585=ORIENTED_EDGE('',*,*,#15458,.F.);
#21586=ORIENTED_EDGE('',*,*,#15455,.F.);
#21587=ORIENTED_EDGE('',*,*,#15540,.F.);
#21588=ORIENTED_EDGE('',*,*,#15541,.T.);
#21589=ORIENTED_EDGE('',*,*,#15537,.T.);
#21590=ORIENTED_EDGE('',*,*,#15534,.T.);
#21591=ORIENTED_EDGE('',*,*,#15531,.T.);
#21592=ORIENTED_EDGE('',*,*,#15528,.T.);
#21593=ORIENTED_EDGE('',*,*,#15525,.T.);
#21594=ORIENTED_EDGE('',*,*,#15522,.T.);
#21595=ORIENTED_EDGE('',*,*,#15519,.T.);
#21596=ORIENTED_EDGE('',*,*,#15516,.T.);
#21597=ORIENTED_EDGE('',*,*,#15513,.T.);
#21598=ORIENTED_EDGE('',*,*,#15510,.T.);
#21599=ORIENTED_EDGE('',*,*,#15507,.T.);
#21600=ORIENTED_EDGE('',*,*,#15504,.T.);
#21601=ORIENTED_EDGE('',*,*,#15501,.T.);
#21602=ORIENTED_EDGE('',*,*,#15498,.T.);
#21603=ORIENTED_EDGE('',*,*,#15542,.T.);
#21604=ORIENTED_EDGE('',*,*,#15543,.T.);
#21605=ORIENTED_EDGE('',*,*,#15544,.T.);
#21606=ORIENTED_EDGE('',*,*,#15545,.T.);
#21607=ORIENTED_EDGE('',*,*,#15540,.T.);
#21608=ORIENTED_EDGE('',*,*,#15535,.T.);
#21609=ORIENTED_EDGE('',*,*,#15541,.F.);
#21610=ORIENTED_EDGE('',*,*,#15545,.F.);
#21611=ORIENTED_EDGE('',*,*,#15546,.T.);
#21612=ORIENTED_EDGE('',*,*,#15547,.F.);
#21613=ORIENTED_EDGE('',*,*,#15496,.F.);
#21614=ORIENTED_EDGE('',*,*,#15500,.F.);
#21615=ORIENTED_EDGE('',*,*,#15503,.F.);
#21616=ORIENTED_EDGE('',*,*,#15506,.F.);
#21617=ORIENTED_EDGE('',*,*,#15509,.F.);
#21618=ORIENTED_EDGE('',*,*,#15512,.F.);
#21619=ORIENTED_EDGE('',*,*,#15515,.F.);
#21620=ORIENTED_EDGE('',*,*,#15518,.F.);
#21621=ORIENTED_EDGE('',*,*,#15521,.F.);
#21622=ORIENTED_EDGE('',*,*,#15524,.F.);
#21623=ORIENTED_EDGE('',*,*,#15527,.F.);
#21624=ORIENTED_EDGE('',*,*,#15530,.F.);
#21625=ORIENTED_EDGE('',*,*,#15533,.F.);
#21626=ORIENTED_EDGE('',*,*,#15536,.F.);
#21627=ORIENTED_EDGE('',*,*,#15546,.F.);
#21628=ORIENTED_EDGE('',*,*,#15544,.F.);
#21629=ORIENTED_EDGE('',*,*,#15453,.F.);
#21630=ORIENTED_EDGE('',*,*,#15457,.F.);
#21631=ORIENTED_EDGE('',*,*,#15460,.F.);
#21632=ORIENTED_EDGE('',*,*,#15463,.F.);
#21633=ORIENTED_EDGE('',*,*,#15466,.F.);
#21634=ORIENTED_EDGE('',*,*,#15469,.F.);
#21635=ORIENTED_EDGE('',*,*,#15472,.F.);
#21636=ORIENTED_EDGE('',*,*,#15475,.F.);
#21637=ORIENTED_EDGE('',*,*,#15478,.F.);
#21638=ORIENTED_EDGE('',*,*,#15481,.F.);
#21639=ORIENTED_EDGE('',*,*,#15484,.F.);
#21640=ORIENTED_EDGE('',*,*,#15487,.F.);
#21641=ORIENTED_EDGE('',*,*,#15490,.F.);
#21642=ORIENTED_EDGE('',*,*,#15493,.F.);
#21643=ORIENTED_EDGE('',*,*,#15548,.F.);
#21644=ORIENTED_EDGE('',*,*,#15538,.T.);
#21645=ORIENTED_EDGE('',*,*,#15497,.T.);
#21646=ORIENTED_EDGE('',*,*,#15547,.T.);
#21647=ORIENTED_EDGE('',*,*,#15549,.T.);
#21648=ORIENTED_EDGE('',*,*,#15550,.F.);
#21649=ORIENTED_EDGE('',*,*,#15551,.F.);
#21650=ORIENTED_EDGE('',*,*,#15552,.T.);
#21651=ORIENTED_EDGE('',*,*,#15553,.T.);
#21652=ORIENTED_EDGE('',*,*,#15554,.F.);
#21653=ORIENTED_EDGE('',*,*,#15555,.F.);
#21654=ORIENTED_EDGE('',*,*,#15556,.T.);
#21655=ORIENTED_EDGE('',*,*,#15557,.T.);
#21656=ORIENTED_EDGE('',*,*,#15552,.F.);
#21657=ORIENTED_EDGE('',*,*,#15558,.F.);
#21658=ORIENTED_EDGE('',*,*,#15559,.T.);
#21659=ORIENTED_EDGE('',*,*,#15560,.T.);
#21660=ORIENTED_EDGE('',*,*,#15556,.F.);
#21661=ORIENTED_EDGE('',*,*,#15561,.F.);
#21662=ORIENTED_EDGE('',*,*,#15562,.T.);
#21663=ORIENTED_EDGE('',*,*,#15563,.T.);
#21664=ORIENTED_EDGE('',*,*,#15559,.F.);
#21665=ORIENTED_EDGE('',*,*,#15564,.F.);
#21666=ORIENTED_EDGE('',*,*,#15565,.T.);
#21667=ORIENTED_EDGE('',*,*,#15566,.T.);
#21668=ORIENTED_EDGE('',*,*,#15562,.F.);
#21669=ORIENTED_EDGE('',*,*,#15567,.F.);
#21670=ORIENTED_EDGE('',*,*,#15554,.T.);
#21671=ORIENTED_EDGE('',*,*,#15568,.T.);
#21672=ORIENTED_EDGE('',*,*,#15565,.F.);
#21673=ORIENTED_EDGE('',*,*,#15568,.F.);
#21674=ORIENTED_EDGE('',*,*,#15553,.F.);
#21675=ORIENTED_EDGE('',*,*,#15557,.F.);
#21676=ORIENTED_EDGE('',*,*,#15560,.F.);
#21677=ORIENTED_EDGE('',*,*,#15563,.F.);
#21678=ORIENTED_EDGE('',*,*,#15566,.F.);
#21679=ORIENTED_EDGE('',*,*,#15569,.F.);
#21680=ORIENTED_EDGE('',*,*,#15551,.T.);
#21681=ORIENTED_EDGE('',*,*,#15567,.T.);
#21682=ORIENTED_EDGE('',*,*,#15564,.T.);
#21683=ORIENTED_EDGE('',*,*,#15561,.T.);
#21684=ORIENTED_EDGE('',*,*,#15558,.T.);
#21685=ORIENTED_EDGE('',*,*,#15555,.T.);
#21686=ORIENTED_EDGE('',*,*,#15542,.F.);
#21687=ORIENTED_EDGE('',*,*,#15454,.F.);
#21688=ORIENTED_EDGE('',*,*,#15543,.F.);
#21689=ORIENTED_EDGE('',*,*,#15570,.T.);
#21690=ORIENTED_EDGE('',*,*,#15569,.T.);
#21691=ORIENTED_EDGE('',*,*,#15570,.F.);
#21692=ORIENTED_EDGE('',*,*,#15492,.T.);
#21693=ORIENTED_EDGE('',*,*,#15539,.T.);
#21694=ORIENTED_EDGE('',*,*,#15549,.F.);
#21695=ORIENTED_EDGE('',*,*,#15548,.T.);
#21696=ORIENTED_EDGE('',*,*,#15571,.F.);
#21697=ORIENTED_EDGE('',*,*,#15572,.T.);
#21698=ORIENTED_EDGE('',*,*,#15550,.T.);
#21699=ORIENTED_EDGE('',*,*,#15572,.F.);
#21700=ORIENTED_EDGE('',*,*,#15573,.F.);
#21701=ORIENTED_EDGE('',*,*,#15574,.T.);
#21702=ORIENTED_EDGE('',*,*,#15571,.T.);
#21703=ORIENTED_EDGE('',*,*,#15574,.F.);
#21704=ORIENTED_EDGE('',*,*,#15573,.T.);
#25068=CONICAL_SURFACE('',#28337,0.37,0.785398163397449);
#25069=CONICAL_SURFACE('',#28341,0.26,0.785398163397448);
#25978=ADVANCED_FACE('',(#3390),#1328,.T.);
#25979=ADVANCED_FACE('',(#3391),#1329,.T.);
#25980=ADVANCED_FACE('',(#3392),#1330,.T.);
#25981=ADVANCED_FACE('',(#3393),#1331,.T.);
#25982=ADVANCED_FACE('',(#3394),#1332,.T.);
#25983=ADVANCED_FACE('',(#3395),#1333,.T.);
#25984=ADVANCED_FACE('',(#3396),#1334,.T.);
#25985=ADVANCED_FACE('',(#3397),#1335,.T.);
#25986=ADVANCED_FACE('',(#3398),#1336,.T.);
#25987=ADVANCED_FACE('',(#3399),#1337,.T.);
#25988=ADVANCED_FACE('',(#3400),#1338,.T.);
#25989=ADVANCED_FACE('',(#3401),#1339,.T.);
#25990=ADVANCED_FACE('',(#3402),#1340,.T.);
#25991=ADVANCED_FACE('',(#3403),#1341,.T.);
#25992=ADVANCED_FACE('',(#3404),#1342,.T.);
#25993=ADVANCED_FACE('',(#3405),#1343,.T.);
#25994=ADVANCED_FACE('',(#3406),#1344,.T.);
#25995=ADVANCED_FACE('',(#3407),#1345,.T.);
#25996=ADVANCED_FACE('',(#3408),#1346,.T.);
#25997=ADVANCED_FACE('',(#3409),#1347,.T.);
#25998=ADVANCED_FACE('',(#3410),#1348,.T.);
#25999=ADVANCED_FACE('',(#3411),#1349,.T.);
#26000=ADVANCED_FACE('',(#3412),#1350,.T.);
#26001=ADVANCED_FACE('',(#3413),#1351,.T.);
#26002=ADVANCED_FACE('',(#3414),#1352,.T.);
#26003=ADVANCED_FACE('',(#3415),#1353,.T.);
#26004=ADVANCED_FACE('',(#3416),#1354,.T.);
#26005=ADVANCED_FACE('',(#3417),#1355,.T.);
#26006=ADVANCED_FACE('',(#3418),#164,.F.);
#26007=ADVANCED_FACE('',(#3419),#2119,.T.);
#26008=ADVANCED_FACE('',(#3420),#1356,.T.);
#26009=ADVANCED_FACE('',(#3421),#165,.F.);
#26010=ADVANCED_FACE('',(#3422,#1638),#2120,.T.);
#26011=ADVANCED_FACE('',(#3423),#2121,.F.);
#26012=ADVANCED_FACE('',(#3424),#2122,.F.);
#26013=ADVANCED_FACE('',(#3425),#2123,.F.);
#26014=ADVANCED_FACE('',(#3426),#2124,.F.);
#26015=ADVANCED_FACE('',(#3427),#2125,.F.);
#26016=ADVANCED_FACE('',(#3428),#2126,.F.);
#26017=ADVANCED_FACE('',(#3429),#2127,.F.);
#26018=ADVANCED_FACE('',(#3430,#1639),#2128,.T.);
#26019=ADVANCED_FACE('',(#3431),#25068,.T.);
#26020=ADVANCED_FACE('',(#3432),#1357,.T.);
#26021=ADVANCED_FACE('',(#3433),#1358,.T.);
#26022=ADVANCED_FACE('',(#3434),#25069,.T.);
#26023=ADVANCED_FACE('',(#3435),#2129,.T.);
#26676=CLOSED_SHELL('',(#25978,#25979,#25980,#25981,#25982,#25983,#25984,
#25985,#25986,#25987,#25988,#25989,#25990,#25991,#25992,#25993,#25994,#25995,
#25996,#25997,#25998,#25999,#26000,#26001,#26002,#26003,#26004,#26005,#26006,
#26007,#26008,#26009,#26010,#26011,#26012,#26013,#26014,#26015,#26016,#26017,
#26018,#26019,#26020,#26021,#26022,#26023));
#28289=AXIS2_PLACEMENT_3D('',#56087,#33328,#33329);
#28290=AXIS2_PLACEMENT_3D('',#56088,#33330,#33331);
#28291=AXIS2_PLACEMENT_3D('',#56104,#33333,#33334);
#28292=AXIS2_PLACEMENT_3D('',#56112,#33335,#33336);
#28293=AXIS2_PLACEMENT_3D('',#56160,#33338,#33339);
#28294=AXIS2_PLACEMENT_3D('',#56208,#33341,#33342);
#28295=AXIS2_PLACEMENT_3D('',#56256,#33344,#33345);
#28296=AXIS2_PLACEMENT_3D('',#56310,#33347,#33348);
#28297=AXIS2_PLACEMENT_3D('',#56358,#33350,#33351);
#28298=AXIS2_PLACEMENT_3D('',#56406,#33353,#33354);
#28299=AXIS2_PLACEMENT_3D('',#56460,#33356,#33357);
#28300=AXIS2_PLACEMENT_3D('',#56508,#33359,#33360);
#28301=AXIS2_PLACEMENT_3D('',#56556,#33362,#33363);
#28302=AXIS2_PLACEMENT_3D('',#56610,#33365,#33366);
#28303=AXIS2_PLACEMENT_3D('',#56658,#33368,#33369);
#28304=AXIS2_PLACEMENT_3D('',#56706,#33371,#33372);
#28305=AXIS2_PLACEMENT_3D('',#56754,#33374,#33375);
#28306=AXIS2_PLACEMENT_3D('',#56766,#33377,#33378);
#28307=AXIS2_PLACEMENT_3D('',#56771,#33379,#33380);
#28308=AXIS2_PLACEMENT_3D('',#56796,#33382,#33383);
#28309=AXIS2_PLACEMENT_3D('',#56820,#33385,#33386);
#28310=AXIS2_PLACEMENT_3D('',#56844,#33388,#33389);
#28311=AXIS2_PLACEMENT_3D('',#56869,#33391,#33392);
#28312=AXIS2_PLACEMENT_3D('',#56894,#33394,#33395);
#28313=AXIS2_PLACEMENT_3D('',#56918,#33397,#33398);
#28314=AXIS2_PLACEMENT_3D('',#56943,#33400,#33401);
#28315=AXIS2_PLACEMENT_3D('',#56968,#33403,#33404);
#28316=AXIS2_PLACEMENT_3D('',#56992,#33406,#33407);
#28317=AXIS2_PLACEMENT_3D('',#57017,#33409,#33410);
#28318=AXIS2_PLACEMENT_3D('',#57042,#33412,#33413);
#28319=AXIS2_PLACEMENT_3D('',#57066,#33415,#33416);
#28320=AXIS2_PLACEMENT_3D('',#57626,#33418,#33419);
#28321=AXIS2_PLACEMENT_3D('',#57628,#33420,#33421);
#28322=AXIS2_PLACEMENT_3D('',#57629,#33422,#33423);
#28323=AXIS2_PLACEMENT_3D('',#57692,#33424,#33425);
#28324=AXIS2_PLACEMENT_3D('',#57693,#33426,#33427);
#28325=AXIS2_PLACEMENT_3D('',#58155,#33428,#33429);
#28326=AXIS2_PLACEMENT_3D('',#58156,#33430,#33431);
#28327=AXIS2_PLACEMENT_3D('',#58158,#33432,#33433);
#28328=AXIS2_PLACEMENT_3D('',#58159,#33434,#33435);
#28329=AXIS2_PLACEMENT_3D('',#58168,#33440,#33441);
#28330=AXIS2_PLACEMENT_3D('',#58174,#33445,#33446);
#28331=AXIS2_PLACEMENT_3D('',#58180,#33450,#33451);
#28332=AXIS2_PLACEMENT_3D('',#58186,#33455,#33456);
#28333=AXIS2_PLACEMENT_3D('',#58192,#33460,#33461);
#28334=AXIS2_PLACEMENT_3D('',#58195,#33464,#33465);
#28335=AXIS2_PLACEMENT_3D('',#58196,#33466,#33467);
#28336=AXIS2_PLACEMENT_3D('',#58198,#33468,#33469);
#28337=AXIS2_PLACEMENT_3D('',#58199,#33470,#33471);
#28338=AXIS2_PLACEMENT_3D('',#58201,#33473,#33474);
#28339=AXIS2_PLACEMENT_3D('',#58202,#33475,#33476);
#28340=AXIS2_PLACEMENT_3D('',#58204,#33477,#33478);
#28341=AXIS2_PLACEMENT_3D('',#58206,#33480,#33481);
#28342=AXIS2_PLACEMENT_3D('',#58208,#33482,#33483);
#28343=AXIS2_PLACEMENT_3D('',#58210,#33485,#33486);
#33328=DIRECTION('axis',(0.,0.,1.));
#33329=DIRECTION('refdir',(1.,0.,0.));
#33330=DIRECTION('center_axis',(0.,0.,1.));
#33331=DIRECTION('ref_axis',(1.,0.,0.));
#33332=DIRECTION('',(0.,0.,-1.));
#33333=DIRECTION('center_axis',(0.,0.,1.));
#33334=DIRECTION('ref_axis',(1.,0.,0.));
#33335=DIRECTION('center_axis',(0.,0.,1.));
#33336=DIRECTION('ref_axis',(1.,0.,0.));
#33337=DIRECTION('',(0.,0.,-1.));
#33338=DIRECTION('center_axis',(0.,0.,1.));
#33339=DIRECTION('ref_axis',(1.,0.,0.));
#33340=DIRECTION('',(0.,0.,-1.));
#33341=DIRECTION('center_axis',(0.,0.,1.));
#33342=DIRECTION('ref_axis',(1.,0.,0.));
#33343=DIRECTION('',(0.,0.,-1.));
#33344=DIRECTION('center_axis',(0.,0.,1.));
#33345=DIRECTION('ref_axis',(1.,0.,0.));
#33346=DIRECTION('',(0.,0.,-1.));
#33347=DIRECTION('center_axis',(0.,0.,1.));
#33348=DIRECTION('ref_axis',(1.,0.,0.));
#33349=DIRECTION('',(0.,0.,-1.));
#33350=DIRECTION('center_axis',(0.,0.,1.));
#33351=DIRECTION('ref_axis',(1.,0.,0.));
#33352=DIRECTION('',(0.,0.,-1.));
#33353=DIRECTION('center_axis',(0.,0.,1.));
#33354=DIRECTION('ref_axis',(1.,0.,0.));
#33355=DIRECTION('',(0.,0.,-1.));
#33356=DIRECTION('center_axis',(0.,0.,1.));
#33357=DIRECTION('ref_axis',(1.,0.,0.));
#33358=DIRECTION('',(0.,0.,-1.));
#33359=DIRECTION('center_axis',(0.,0.,1.));
#33360=DIRECTION('ref_axis',(1.,0.,0.));
#33361=DIRECTION('',(0.,0.,-1.));
#33362=DIRECTION('center_axis',(0.,0.,1.));
#33363=DIRECTION('ref_axis',(1.,0.,0.));
#33364=DIRECTION('',(0.,0.,-1.));
#33365=DIRECTION('center_axis',(0.,0.,1.));
#33366=DIRECTION('ref_axis',(1.,0.,0.));
#33367=DIRECTION('',(0.,0.,-1.));
#33368=DIRECTION('center_axis',(0.,0.,1.));
#33369=DIRECTION('ref_axis',(1.,0.,0.));
#33370=DIRECTION('',(0.,0.,-1.));
#33371=DIRECTION('center_axis',(0.,0.,1.));
#33372=DIRECTION('ref_axis',(1.,0.,0.));
#33373=DIRECTION('',(0.,0.,-1.));
#33374=DIRECTION('center_axis',(0.,0.,1.));
#33375=DIRECTION('ref_axis',(-0.530268055707691,-0.847830047294849,0.));
#33376=DIRECTION('',(0.,0.,1.));
#33377=DIRECTION('center_axis',(0.,0.,1.));
#33378=DIRECTION('ref_axis',(1.,9.13482547654578E-14,0.));
#33379=DIRECTION('center_axis',(0.,0.,1.));
#33380=DIRECTION('ref_axis',(1.,9.13482547654578E-14,0.));
#33381=DIRECTION('',(0.,0.,1.));
#33382=DIRECTION('center_axis',(0.,0.,1.));
#33383=DIRECTION('ref_axis',(1.,9.13482547654578E-14,0.));
#33384=DIRECTION('',(0.,0.,1.));
#33385=DIRECTION('center_axis',(0.,0.,1.));
#33386=DIRECTION('ref_axis',(1.,9.13482547654578E-14,0.));
#33387=DIRECTION('',(0.,0.,1.));
#33388=DIRECTION('center_axis',(0.,0.,1.));
#33389=DIRECTION('ref_axis',(1.,9.13482547654578E-14,0.));
#33390=DIRECTION('',(0.,0.,1.));
#33391=DIRECTION('center_axis',(0.,0.,1.));
#33392=DIRECTION('ref_axis',(1.,9.13482547654578E-14,0.));
#33393=DIRECTION('',(0.,0.,1.));
#33394=DIRECTION('center_axis',(0.,0.,1.));
#33395=DIRECTION('ref_axis',(1.,9.13482547654578E-14,0.));
#33396=DIRECTION('',(0.,0.,1.));
#33397=DIRECTION('center_axis',(0.,0.,1.));
#33398=DIRECTION('ref_axis',(1.,9.13482547654578E-14,0.));
#33399=DIRECTION('',(0.,0.,1.));
#33400=DIRECTION('center_axis',(0.,0.,1.));
#33401=DIRECTION('ref_axis',(1.,9.13482547654578E-14,0.));
#33402=DIRECTION('',(0.,0.,1.));
#33403=DIRECTION('center_axis',(0.,0.,1.));
#33404=DIRECTION('ref_axis',(1.,9.13482547654578E-14,0.));
#33405=DIRECTION('',(0.,0.,1.));
#33406=DIRECTION('center_axis',(0.,0.,1.));
#33407=DIRECTION('ref_axis',(1.,9.13482547654578E-14,0.));
#33408=DIRECTION('',(0.,0.,1.));
#33409=DIRECTION('center_axis',(0.,0.,1.));
#33410=DIRECTION('ref_axis',(1.,9.13482547654578E-14,0.));
#33411=DIRECTION('',(0.,0.,1.));
#33412=DIRECTION('center_axis',(0.,0.,1.));
#33413=DIRECTION('ref_axis',(1.,9.13482547654578E-14,0.));
#33414=DIRECTION('',(0.,0.,1.));
#33415=DIRECTION('center_axis',(0.,0.,1.));
#33416=DIRECTION('ref_axis',(1.,9.13482547654578E-14,0.));
#33417=DIRECTION('',(0.,0.,1.));
#33418=DIRECTION('center_axis',(0.,0.,1.));
#33419=DIRECTION('ref_axis',(1.,0.,0.));
#33420=DIRECTION('center_axis',(0.,0.,1.));
#33421=DIRECTION('ref_axis',(1.,0.,0.));
#33422=DIRECTION('center_axis',(0.,0.,1.));
#33423=DIRECTION('ref_axis',(1.,0.,0.));
#33424=DIRECTION('center_axis',(0.,0.,-1.));
#33425=DIRECTION('ref_axis',(1.,9.13482547654578E-14,0.));
#33426=DIRECTION('center_axis',(0.,0.,1.));
#33427=DIRECTION('ref_axis',(1.,9.13482547654578E-14,0.));
#33428=DIRECTION('center_axis',(0.,0.,1.));
#33429=DIRECTION('ref_axis',(1.,0.,0.));
#33430=DIRECTION('center_axis',(0.,0.,-1.));
#33431=DIRECTION('ref_axis',(1.,0.,0.));
#33432=DIRECTION('center_axis',(0.,0.,1.));
#33433=DIRECTION('ref_axis',(1.,0.,0.));
#33434=DIRECTION('center_axis',(-2.40370335797945E-16,-1.,0.));
#33435=DIRECTION('ref_axis',(1.,-2.40370335797945E-16,0.));
#33436=DIRECTION('',(1.,-2.40370335797945E-16,0.));
#33437=DIRECTION('',(0.,0.,1.));
#33438=DIRECTION('',(1.,-2.40370335797945E-16,0.));
#33439=DIRECTION('',(0.,0.,1.));
#33440=DIRECTION('center_axis',(-0.866025403784439,-0.5,0.));
#33441=DIRECTION('ref_axis',(0.5,-0.866025403784439,0.));
#33442=DIRECTION('',(0.5,-0.866025403784439,0.));
#33443=DIRECTION('',(0.,0.,1.));
#33444=DIRECTION('',(0.5,-0.866025403784439,0.));
#33445=DIRECTION('center_axis',(-0.866025403784439,0.5,0.));
#33446=DIRECTION('ref_axis',(-0.5,-0.866025403784439,0.));
#33447=DIRECTION('',(-0.5,-0.866025403784439,0.));
#33448=DIRECTION('',(0.,0.,1.));
#33449=DIRECTION('',(-0.5,-0.866025403784439,0.));
#33450=DIRECTION('center_axis',(1.20185167898973E-16,1.,0.));
#33451=DIRECTION('ref_axis',(-1.,1.20185167898973E-16,0.));
#33452=DIRECTION('',(-1.,1.20185167898973E-16,0.));
#33453=DIRECTION('',(0.,0.,1.));
#33454=DIRECTION('',(-1.,1.20185167898973E-16,0.));
#33455=DIRECTION('center_axis',(0.866025403784439,0.5,0.));
#33456=DIRECTION('ref_axis',(-0.5,0.866025403784439,0.));
#33457=DIRECTION('',(-0.5,0.866025403784439,0.));
#33458=DIRECTION('',(0.,0.,1.));
#33459=DIRECTION('',(-0.5,0.866025403784439,0.));
#33460=DIRECTION('center_axis',(0.866025403784439,-0.5,0.));
#33461=DIRECTION('ref_axis',(0.5,0.866025403784439,0.));
#33462=DIRECTION('',(0.5,0.866025403784439,0.));
#33463=DIRECTION('',(0.5,0.866025403784439,0.));
#33464=DIRECTION('center_axis',(0.,0.,1.));
#33465=DIRECTION('ref_axis',(1.,0.,0.));
#33466=DIRECTION('center_axis',(0.,0.,-1.));
#33467=DIRECTION('ref_axis',(-1.,0.,0.));
#33468=DIRECTION('center_axis',(0.,0.,1.));
#33469=DIRECTION('ref_axis',(1.,0.,0.));
#33470=DIRECTION('center_axis',(0.,0.,1.));
#33471=DIRECTION('ref_axis',(1.,0.,0.));
#33472=DIRECTION('',(0.707106781186548,8.65956056235494E-17,-0.707106781186547));
#33473=DIRECTION('center_axis',(0.,0.,1.));
#33474=DIRECTION('ref_axis',(1.,0.,0.));
#33475=DIRECTION('center_axis',(0.,0.,1.));
#33476=DIRECTION('ref_axis',(1.,0.,0.));
#33477=DIRECTION('center_axis',(0.,0.,1.));
#33478=DIRECTION('ref_axis',(1.,0.,0.));
#33479=DIRECTION('',(0.,0.,-1.));
#33480=DIRECTION('center_axis',(0.,0.,-1.));
#33481=DIRECTION('ref_axis',(1.,0.,0.));
#33482=DIRECTION('center_axis',(0.,0.,1.));
#33483=DIRECTION('ref_axis',(1.,0.,0.));
#33484=DIRECTION('',(-0.707106781186547,-8.65956056235493E-17,-0.707106781186548));
#33485=DIRECTION('center_axis',(0.,0.,1.));
#33486=DIRECTION('ref_axis',(1.,0.,0.));
#56087=CARTESIAN_POINT('',(0.,0.,0.));
#56088=CARTESIAN_POINT('Origin',(0.,0.,0.93));
#56089=CARTESIAN_POINT('',(-0.393785571917083,0.000248495837930046,0.0937163522034969));
#56090=CARTESIAN_POINT('',(-0.393691807349815,0.000401671216108742,0.0753836477965013));
#56091=CARTESIAN_POINT('',(-0.3933,-4.81653586104654E-17,0.93));
#56092=CARTESIAN_POINT('',(0.175074770038262,0.352555242519502,0.0533));
#56093=CARTESIAN_POINT('Ctrl Pts',(-0.393785571917083,0.000248495837930046,
0.0937163522034969));
#56094=CARTESIAN_POINT('Ctrl Pts',(-0.393873138151706,0.0131776353947525,
0.0930600049995511));
#56095=CARTESIAN_POINT('Ctrl Pts',(-0.393291866198186,0.0260982907353025,
0.0924036577956053));
#56096=CARTESIAN_POINT('Ctrl Pts',(-0.392015953470318,0.038949338819979,
0.0917473105916596));
#56097=CARTESIAN_POINT('Ctrl Pts',(-0.379144732760665,0.168588829543332,
0.0851261761365885));
#56098=CARTESIAN_POINT('Ctrl Pts',(-0.295583540395456,0.29114475257756,
0.0785050416815174));
#56099=CARTESIAN_POINT('Ctrl Pts',(-0.179607489182299,0.350585393928814,
0.0718839072264463));
#56100=CARTESIAN_POINT('Ctrl Pts',(-0.071102006178845,0.40619718129687,
0.0656892714842975));
#56101=CARTESIAN_POINT('Ctrl Pts',(0.0657768433630953,0.406562915311091,
0.0594946357421488));
#56102=CARTESIAN_POINT('Ctrl Pts',(0.175280092543415,0.352824285593914,
0.0533));
#56103=CARTESIAN_POINT('',(-0.174869447533114,0.352286199445087,0.0533));
#56104=CARTESIAN_POINT('Origin',(0.,0.,0.0533));
#56105=CARTESIAN_POINT('Ctrl Pts',(-0.174869447533113,0.352286199445087,
0.0533000000000003));
#56106=CARTESIAN_POINT('Ctrl Pts',(-0.292115409128919,0.294087108586454,
0.0599211344550713));
#56107=CARTESIAN_POINT('Ctrl Pts',(-0.377001626803167,0.173250680215973,
0.0665422689101422));
#56108=CARTESIAN_POINT('Ctrl Pts',(-0.391451042526116,0.0439776134704028,
0.0731634033652133));
#56109=CARTESIAN_POINT('Ctrl Pts',(-0.393066135076189,0.0295280349525525,
0.0739034848423093));
#56110=CARTESIAN_POINT('Ctrl Pts',(-0.393801204906527,0.0149730508336159,
0.0746435663194053));
#56111=CARTESIAN_POINT('Ctrl Pts',(-0.393691807349815,0.000401671216108742,
0.0753836477965013));
#56112=CARTESIAN_POINT('Origin',(0.,0.,0.93));
#56113=CARTESIAN_POINT('',(-0.392774766082733,0.000218508532499828,0.218716352203497));
#56114=CARTESIAN_POINT('',(-0.392747480256298,0.000198404254828114,0.200383647796502));
#56115=CARTESIAN_POINT('',(-0.3933,-4.81653586104654E-17,0.93));
#56116=CARTESIAN_POINT('Ctrl Pts',(-0.392774766082733,0.000218508532499828,
0.218716352203497));
#56117=CARTESIAN_POINT('Ctrl Pts',(-0.393033682673394,0.0517027350259926,
0.216120145063311));
#56118=CARTESIAN_POINT('Ctrl Pts',(-0.383636180758456,0.103096084244051,
0.213523937923125));
#56119=CARTESIAN_POINT('Ctrl Pts',(-0.364141337824362,0.150320959570902,
0.210927730782939));
#56120=CARTESIAN_POINT('Ctrl Pts',(-0.314423434252966,0.270759057256997,
0.204306596327868));
#56121=CARTESIAN_POINT('Ctrl Pts',(-0.19903157760138,0.36408505105081,0.197685461872797));
#56122=CARTESIAN_POINT('Ctrl Pts',(-0.0708595116212159,0.3875222920239,
0.191064327417726));
#56123=CARTESIAN_POINT('Ctrl Pts',(0.0573125543589477,0.41095953299699,
0.184443192962655));
#56124=CARTESIAN_POINT('Ctrl Pts',(0.198264829667689,0.364508021149357,
0.177822058507584));
#56125=CARTESIAN_POINT('Ctrl Pts',(0.287385293506548,0.269454991498079,
0.171200924052513));
#56126=CARTESIAN_POINT('Ctrl Pts',(0.376505757345406,0.174401961846802,
0.164579789597442));
#56127=CARTESIAN_POINT('Ctrl Pts',(0.413794409714382,0.030747414391879,
0.157958655142371));
#56128=CARTESIAN_POINT('Ctrl Pts',(0.38216066130072,-0.0956482825730319,
0.151337520687299));
#56129=CARTESIAN_POINT('Ctrl Pts',(0.350526912887059,-0.222043979537944,
0.144716386232228));
#56130=CARTESIAN_POINT('Ctrl Pts',(0.249970763690759,-0.331180826012843,
0.138095251777157));
#56131=CARTESIAN_POINT('Ctrl Pts',(0.126581974628838,-0.373052348623724,
0.131474117322086));
#56132=CARTESIAN_POINT('Ctrl Pts',(0.0031931855669175,-0.414923871234605,
0.124852982867015));
#56133=CARTESIAN_POINT('Ctrl Pts',(-0.143028243360624,-0.389530069981469,
0.118231848411944));
#56134=CARTESIAN_POINT('Ctrl Pts',(-0.245048333297346,-0.308471640148661,
0.111610713956873));
#56135=CARTESIAN_POINT('Ctrl Pts',(-0.336955261927553,-0.235448460791133,
0.105645926705748));
#56136=CARTESIAN_POINT('Ctrl Pts',(-0.392989782803075,-0.117249630661176,
0.0996811394546222));
#56137=CARTESIAN_POINT('Ctrl Pts',(-0.393785571917083,0.000248495837930046,
0.0937163522034969));
#56138=CARTESIAN_POINT('Ctrl Pts',(-0.393691807349815,0.000401671216108742,
0.0753836477965013));
#56139=CARTESIAN_POINT('Ctrl Pts',(-0.392822480327593,-0.115389708712764,
0.0812647007744764));
#56140=CARTESIAN_POINT('Ctrl Pts',(-0.338627768779739,-0.23221641135412,
0.0871457537524516));
#56141=CARTESIAN_POINT('Ctrl Pts',(-0.248949174886101,-0.305413577230776,
0.0930268067304266));
#56142=CARTESIAN_POINT('Ctrl Pts',(-0.147985277751488,-0.387821996065721,
0.0996479411854977));
#56143=CARTESIAN_POINT('Ctrl Pts',(-0.00204486971061162,-0.414929128614953,
0.106269075640569));
#56144=CARTESIAN_POINT('Ctrl Pts',(0.121875108290386,-0.374587115506913,
0.11289021009564));
#56145=CARTESIAN_POINT('Ctrl Pts',(0.245795086291383,-0.334245102398874,
0.119511344550711));
#56146=CARTESIAN_POINT('Ctrl Pts',(0.347694634252502,-0.226453943633564,
0.126132479005782));
#56147=CARTESIAN_POINT('Ctrl Pts',(0.380915425583095,-0.100483894323947,
0.132753613460853));
#56148=CARTESIAN_POINT('Ctrl Pts',(0.414136216913688,0.0254861549856705,
0.139374747915924));
#56149=CARTESIAN_POINT('Ctrl Pts',(0.378678251613755,0.169635094839595,
0.145995882370995));
#56150=CARTESIAN_POINT('Ctrl Pts',(0.290768388774417,0.26581421567225,0.152617016826066));
#56151=CARTESIAN_POINT('Ctrl Pts',(0.20285852593508,0.361993336504906,0.159238151281137));
#56152=CARTESIAN_POINT('Ctrl Pts',(0.0624967655563389,0.410202638316291,
0.165859285736208));
#56153=CARTESIAN_POINT('Ctrl Pts',(-0.0659627539324038,0.388381262159473,
0.17248042019128));
#56154=CARTESIAN_POINT('Ctrl Pts',(-0.194422273421146,0.366559886002655,
0.179101554646351));
#56155=CARTESIAN_POINT('Ctrl Pts',(-0.310979552019891,0.274707831877633,
0.185722689101422));
#56156=CARTESIAN_POINT('Ctrl Pts',(-0.362213305892249,0.15490936366835,
0.192343823556493));
#56157=CARTESIAN_POINT('Ctrl Pts',(-0.382950455952394,0.106420259816605,
0.195023764969829));
#56158=CARTESIAN_POINT('Ctrl Pts',(-0.392985841361541,0.0533527755479766,
0.197703706383165));
#56159=CARTESIAN_POINT('Ctrl Pts',(-0.392747480256298,0.000198404254828114,
0.200383647796502));
#56160=CARTESIAN_POINT('Origin',(0.,0.,0.93));
#56161=CARTESIAN_POINT('',(-0.392993347059397,-0.000324654934744873,0.343716352203497));
#56162=CARTESIAN_POINT('',(-0.393037056464261,-0.000335938643299616,0.325383647796502));
#56163=CARTESIAN_POINT('',(-0.3933,-4.81653586104654E-17,0.93));
#56164=CARTESIAN_POINT('Ctrl Pts',(-0.392993347059397,-0.000324654934744872,
0.343716352203497));
#56165=CARTESIAN_POINT('Ctrl Pts',(-0.392295244312066,0.089502206410554,
0.339180285127071));
#56166=CARTESIAN_POINT('Ctrl Pts',(-0.361732461003469,0.179758489715605,
0.334644218050645));
#56167=CARTESIAN_POINT('Ctrl Pts',(-0.305324449239513,0.248942199255532,
0.330108150974219));
#56168=CARTESIAN_POINT('Ctrl Pts',(-0.222987697172201,0.349927179249557,
0.323487016519147));
#56169=CARTESIAN_POINT('Ctrl Pts',(-0.0855845998030076,0.406014524643294,
0.316865882064077));
#56170=CARTESIAN_POINT('Ctrl Pts',(0.0439008348702589,0.391494492203043,
0.310244747609005));
#56171=CARTESIAN_POINT('Ctrl Pts',(0.173386269543525,0.376974459762792,
0.303623613153934));
#56172=CARTESIAN_POINT('Ctrl Pts',(0.294954041520864,0.291847049488554,
0.297002478698863));
#56173=CARTESIAN_POINT('Ctrl Pts',(0.352878842457608,0.175133586498971,
0.290381344243792));
#56174=CARTESIAN_POINT('Ctrl Pts',(0.410803643394352,0.0584201235093882,
0.283760209788721));
#56175=CARTESIAN_POINT('Ctrl Pts',(0.4050854732905,-0.0898793921955392,
0.27713907533365));
#56176=CARTESIAN_POINT('Ctrl Pts',(0.338345518826343,-0.201785929869207,
0.270517940878579));
#56177=CARTESIAN_POINT('Ctrl Pts',(0.271605564362186,-0.313692467542874,
0.263896806423508));
#56178=CARTESIAN_POINT('Ctrl Pts',(0.143843825537725,-0.389206027185282,
0.257275671968437));
#56179=CARTESIAN_POINT('Ctrl Pts',(0.0136247512769219,-0.393712466080529,
0.250654537513365));
#56180=CARTESIAN_POINT('Ctrl Pts',(-0.116594322983881,-0.398218904975776,
0.244033403058294));
#56181=CARTESIAN_POINT('Ctrl Pts',(-0.249270732681025,-0.331718223123861,
0.237412268603223));
#56182=CARTESIAN_POINT('Ctrl Pts',(-0.323586962283995,-0.224692781408716,
0.230791134148152));
#56183=CARTESIAN_POINT('Ctrl Pts',(-0.368763121218386,-0.159632990421233,
0.226766206833267));
#56184=CARTESIAN_POINT('Ctrl Pts',(-0.392373364961114,-0.0795980308691116,
0.222741279518382));
#56185=CARTESIAN_POINT('Ctrl Pts',(-0.392774766082733,0.000218508532499828,
0.218716352203497));
#56186=CARTESIAN_POINT('Ctrl Pts',(-0.392747480256298,0.000198404254828114,
0.200383647796502));
#56187=CARTESIAN_POINT('Ctrl Pts',(-0.392396940082276,-0.077971826346426,
0.204324840838236));
#56188=CARTESIAN_POINT('Ctrl Pts',(-0.369826931677392,-0.156329971208392,
0.208266033879971));
#56189=CARTESIAN_POINT('Ctrl Pts',(-0.326398803783175,-0.220590446720741,
0.212207226921706));
#56190=CARTESIAN_POINT('Ctrl Pts',(-0.253440318655772,-0.328546906607003,
0.218828361376777));
#56191=CARTESIAN_POINT('Ctrl Pts',(-0.121613119254995,-0.396714944085984,
0.225449495831848));
#56192=CARTESIAN_POINT('Ctrl Pts',(0.00865273155690482,-0.393852455738489,
0.232070630286919));
#56193=CARTESIAN_POINT('Ctrl Pts',(0.138918582368805,-0.390989967390994,
0.23869176474199));
#56194=CARTESIAN_POINT('Ctrl Pts',(0.267623084591827,-0.317096953217022,
0.245312899197062));
#56195=CARTESIAN_POINT('Ctrl Pts',(0.335770584171616,-0.206042341202286,
0.251934033652133));
#56196=CARTESIAN_POINT('Ctrl Pts',(0.403918083751406,-0.0949877291875496,
0.258555168107204));
#56197=CARTESIAN_POINT('Ctrl Pts',(0.411508580687962,0.0532284806679498,
0.265176302562275));
#56198=CARTESIAN_POINT('Ctrl Pts',(0.355062141117544,0.170664205462423,
0.271797437017346));
#56199=CARTESIAN_POINT('Ctrl Pts',(0.298615701547127,0.288099930256896,
0.278418571472417));
#56200=CARTESIAN_POINT('Ctrl Pts',(0.178132325469737,0.374755169990342,
0.285039705927488));
#56201=CARTESIAN_POINT('Ctrl Pts',(0.0488405039998853,0.390908905805843,
0.291660840382559));
#56202=CARTESIAN_POINT('Ctrl Pts',(-0.0804513174699659,0.407062641621344,
0.29828197483763));
#56203=CARTESIAN_POINT('Ctrl Pts',(-0.218551584332279,0.352714873518899,
0.304903109292701));
#56204=CARTESIAN_POINT('Ctrl Pts',(-0.302156848319226,0.252777605399255,
0.311524243747772));
#56205=CARTESIAN_POINT('Ctrl Pts',(-0.360491218965147,0.183047813735153,
0.316144045097349));
#56206=CARTESIAN_POINT('Ctrl Pts',(-0.392295515188098,0.0911234580827075,
0.320763846446925));
#56207=CARTESIAN_POINT('Ctrl Pts',(-0.393037056464261,-0.000335938643299616,
0.325383647796502));
#56208=CARTESIAN_POINT('Origin',(0.,0.,0.93));
#56209=CARTESIAN_POINT('',(-0.393939358387839,-5.33598371626476E-5,0.468716352203497));
#56210=CARTESIAN_POINT('',(-0.39394666710269,-2.26739104671677E-5,0.450383647796501));
#56211=CARTESIAN_POINT('',(-0.3933,-4.81653586104654E-17,0.93));
#56212=CARTESIAN_POINT('Ctrl Pts',(-0.393939358387839,-5.33598371626476E-5,
0.468716352203497));
#56213=CARTESIAN_POINT('Ctrl Pts',(-0.393697045666046,0.127393873184695,
0.462240425190831));
#56214=CARTESIAN_POINT('Ctrl Pts',(-0.326158936027309,0.255061565108686,
0.455764498178165));
#56215=CARTESIAN_POINT('Ctrl Pts',(-0.220566552565224,0.326413281704456,
0.449288571165498));
#56216=CARTESIAN_POINT('Ctrl Pts',(-0.112606508085655,0.399364892841627,
0.442667436710427));
#56217=CARTESIAN_POINT('Ctrl Pts',(0.0351334982603933,0.413446707607708,
0.436046302255356));
#56218=CARTESIAN_POINT('Ctrl Pts',(0.15493112546501,0.362203783209636,0.429425167800285));
#56219=CARTESIAN_POINT('Ctrl Pts',(0.274728752669627,0.310960858811565,
0.422804033345214));
#56220=CARTESIAN_POINT('Ctrl Pts',(0.366584000732812,0.194393195249342,
0.416182898890143));
#56221=CARTESIAN_POINT('Ctrl Pts',(0.388391466562617,0.0659340835312544,
0.409561764435072));
#56222=CARTESIAN_POINT('Ctrl Pts',(0.410198932392422,-0.0625250281868314,
0.402940629980001));
#56223=CARTESIAN_POINT('Ctrl Pts',(0.361958615988848,-0.202875588060781,
0.39631949552493));
#56224=CARTESIAN_POINT('Ctrl Pts',(0.265783331451548,-0.290782488832414,
0.389698361069858));
#56225=CARTESIAN_POINT('Ctrl Pts',(0.169608046914247,-0.378689389604048,
0.383077226614787));
#56226=CARTESIAN_POINT('Ctrl Pts',(0.0254977942432194,-0.414152631273365,
0.376456092159716));
#56227=CARTESIAN_POINT('Ctrl Pts',(-0.100488924827274,-0.380916274938763,
0.369834957704645));
#56228=CARTESIAN_POINT('Ctrl Pts',(-0.226475643897767,-0.347679918604161,
0.363213823249574));
#56229=CARTESIAN_POINT('Ctrl Pts',(-0.334338829367725,-0.24574396426564,
0.356592688794503));
#56230=CARTESIAN_POINT('Ctrl Pts',(-0.374635218719989,-0.121834679799224,
0.349971554339432));
#56231=CARTESIAN_POINT('Ctrl Pts',(-0.387324990765207,-0.0828142961013362,
0.347886486960787));
#56232=CARTESIAN_POINT('Ctrl Pts',(-0.393314239859455,-0.0416148420421024,
0.345801419582142));
#56233=CARTESIAN_POINT('Ctrl Pts',(-0.392993347059397,-0.000324654934744872,
0.343716352203497));
#56234=CARTESIAN_POINT('Ctrl Pts',(-0.393037056464261,-0.000335938643299616,
0.325383647796502));
#56235=CARTESIAN_POINT('Ctrl Pts',(-0.393358297788893,-0.0399568453935667,
0.327384980901996));
#56236=CARTESIAN_POINT('Ctrl Pts',(-0.387850028107362,-0.0794904938441846,
0.329386314007491));
#56237=CARTESIAN_POINT('Ctrl Pts',(-0.376143742454461,-0.117094674587401,
0.331387647112986));
#56238=CARTESIAN_POINT('Ctrl Pts',(-0.337415111491167,-0.241502918317571,
0.338008781568057));
#56239=CARTESIAN_POINT('Ctrl Pts',(-0.230847588452996,-0.344792637641065,
0.344629916023128));
#56240=CARTESIAN_POINT('Ctrl Pts',(-0.105290555440245,-0.379617105798059,
0.351251050478199));
#56241=CARTESIAN_POINT('Ctrl Pts',(0.0202664775725054,-0.414441573955053,
0.35787218493327));
#56242=CARTESIAN_POINT('Ctrl Pts',(0.164813020559835,-0.380800790945546,
0.364493319388341));
#56243=CARTESIAN_POINT('Ctrl Pts',(0.262090600311147,-0.294115253540458,
0.371114453843412));
#56244=CARTESIAN_POINT('Ctrl Pts',(0.359368180062459,-0.20742971613537,
0.377735588298483));
#56245=CARTESIAN_POINT('Ctrl Pts',(0.409376796577753,-0.0676994243346997,
0.384356722753555));
#56246=CARTESIAN_POINT('Ctrl Pts',(0.389193057131155,0.0610248135294344,
0.390977857208626));
#56247=CARTESIAN_POINT('Ctrl Pts',(0.369009317684557,0.189749051393568,
0.397598991663697));
#56248=CARTESIAN_POINT('Ctrl Pts',(0.278633222276068,0.307467235321165,
0.404220126118768));
#56249=CARTESIAN_POINT('Ctrl Pts',(0.159492152398559,0.36021870182656,0.410841260573839));
#56250=CARTESIAN_POINT('Ctrl Pts',(0.0403510825210511,0.412970168331956,
0.41746239502891));
#56251=CARTESIAN_POINT('Ctrl Pts',(-0.107554961825477,0.400754917415149,
0.424083529483981));
#56252=CARTESIAN_POINT('Ctrl Pts',(-0.21642753240124,0.329172273420514,
0.430704663939052));
#56253=CARTESIAN_POINT('Ctrl Pts',(-0.324289287986974,0.258254230336771,
0.437264325224869));
#56254=CARTESIAN_POINT('Ctrl Pts',(-0.393839008812417,0.1290660563243,0.443823986510685));
#56255=CARTESIAN_POINT('Ctrl Pts',(-0.39394666710269,-2.26739104671677E-5,
0.450383647796501));
#56256=CARTESIAN_POINT('Origin',(0.,0.,0.93));
#56257=CARTESIAN_POINT('',(-0.393151626951805,0.000355166996054868,0.593716352203497));
#56258=CARTESIAN_POINT('',(-0.393104204086639,0.000348908879909379,0.575383647796501));
#56259=CARTESIAN_POINT('',(-0.3933,-4.81653586104654E-17,0.93));
#56260=CARTESIAN_POINT('Ctrl Pts',(-0.393151626951805,0.000355166996054868,
0.593716352203497));
#56261=CARTESIAN_POINT('Ctrl Pts',(-0.39346294402003,0.0358581068632945,
0.591921699709662));
#56262=CARTESIAN_POINT('Ctrl Pts',(-0.389051359657766,0.0712850359655204,
0.590127047215827));
#56263=CARTESIAN_POINT('Ctrl Pts',(-0.3796098892593,0.105316506102462,0.588332394721991));
#56264=CARTESIAN_POINT('Ctrl Pts',(-0.344776825378376,0.230871141473065,
0.58171126026692));
#56265=CARTESIAN_POINT('Ctrl Pts',(-0.241479768298012,0.337431570529307,
0.575090125811849));
#56266=CARTESIAN_POINT('Ctrl Pts',(-0.11706891599188,0.376151702631086,
0.568468991356778));
#56267=CARTESIAN_POINT('Ctrl Pts',(0.00734193631425342,0.414871834732865,
0.561847856901707));
#56268=CARTESIAN_POINT('Ctrl Pts',(0.152866583846155,0.38575166988018,0.555226722446636));
#56269=CARTESIAN_POINT('Ctrl Pts',(0.252798180691623,0.302139560990116,
0.548605587991565));
#56270=CARTESIAN_POINT('Ctrl Pts',(0.35272977753709,0.218527452100053,0.541984453536493));
#56271=CARTESIAN_POINT('Ctrl Pts',(0.407068323696124,0.0804233991726108,
0.535363319081422));
#56272=CARTESIAN_POINT('Ctrl Pts',(0.390905646644255,-0.0488672682230429,
0.528742184626351));
#56273=CARTESIAN_POINT('Ctrl Pts',(0.374742969592385,-0.178157935618697,
0.52212105017128));
#56274=CARTESIAN_POINT('Ctrl Pts',(0.28807906932961,-0.298635217482562,
0.515499915716209));
#56275=CARTESIAN_POINT('Ctrl Pts',(0.170639693637779,-0.355073695805415,
0.508878781261138));
#56276=CARTESIAN_POINT('Ctrl Pts',(0.0532003179459488,-0.411512174128268,
0.502257646806067));
#56277=CARTESIAN_POINT('Ctrl Pts',(-0.095014533174937,-0.403911848910109,
0.495636512350996));
#56278=CARTESIAN_POINT('Ctrl Pts',(-0.206064855064571,-0.335756623093911,
0.489015377895925));
#56279=CARTESIAN_POINT('Ctrl Pts',(-0.317115176954206,-0.267601397277712,
0.482394243440854));
#56280=CARTESIAN_POINT('Ctrl Pts',(-0.39100096961259,-0.138891270863474,
0.475773108985783));
#56281=CARTESIAN_POINT('Ctrl Pts',(-0.393853824635236,-0.00862550390222436,
0.469151974530712));
#56282=CARTESIAN_POINT('Ctrl Pts',(-0.393916390315514,-0.00576865829944947,
0.469006767088307));
#56283=CARTESIAN_POINT('Ctrl Pts',(-0.393944791681099,-0.00291106448894218,
0.468861559645902));
#56284=CARTESIAN_POINT('Ctrl Pts',(-0.393939358387839,-5.33598371626476E-5,
0.468716352203497));
#56285=CARTESIAN_POINT('Ctrl Pts',(-0.39394666710269,-2.26739104671677E-5,
0.450383647796501));
#56286=CARTESIAN_POINT('Ctrl Pts',(-0.393947676010927,-0.00123241523960264,
0.450445120965756));
#56287=CARTESIAN_POINT('Ctrl Pts',(-0.393942586307364,-0.00244214783528503,
0.45050659413501));
#56288=CARTESIAN_POINT('Ctrl Pts',(-0.39393137237124,-0.00365182365794601,
0.450568067304265));
#56289=CARTESIAN_POINT('Ctrl Pts',(-0.392723544960477,-0.133943239669311,
0.457189201759336));
#56290=CARTESIAN_POINT('Ctrl Pts',(-0.320468793333952,-0.263576034619581,
0.463810336214408));
#56291=CARTESIAN_POINT('Ctrl Pts',(-0.210287875943413,-0.333128009521044,
0.470431470669479));
#56292=CARTESIAN_POINT('Ctrl Pts',(-0.100106958552874,-0.402679984422508,
0.47705260512455));
#56293=CARTESIAN_POINT('Ctrl Pts',(0.0480001246016787,-0.412151139275165,
0.483673739579621));
#56294=CARTESIAN_POINT('Ctrl Pts',(0.166142768855205,-0.357200003114843,
0.490294874034692));
#56295=CARTESIAN_POINT('Ctrl Pts',(0.28428541310873,-0.302248866954521,
0.496916008489763));
#56296=CARTESIAN_POINT('Ctrl Pts',(0.372463618461229,-0.18287543978122,
0.503537142944834));
#56297=CARTESIAN_POINT('Ctrl Pts',(0.390257496673607,-0.0537991456500621,
0.510158277399905));
#56298=CARTESIAN_POINT('Ctrl Pts',(0.408051374885984,0.0752771484810965,
0.516779411854976));
#56299=CARTESIAN_POINT('Ctrl Pts',(0.355460925958238,0.214056309570112,
0.523400546310047));
#56300=CARTESIAN_POINT('Ctrl Pts',(0.256593014598855,0.298923546394139,
0.530021680765118));
#56301=CARTESIAN_POINT('Ctrl Pts',(0.157725103239472,0.383790783218166,
0.536642815220189));
#56302=CARTESIAN_POINT('Ctrl Pts',(0.0125797294484521,0.414746095777205,
0.54326394967526));
#56303=CARTESIAN_POINT('Ctrl Pts',(-0.112310115692326,0.37759992014838,
0.549885084130332));
#56304=CARTESIAN_POINT('Ctrl Pts',(-0.237199960833103,0.340453744519554,
0.556506218585403));
#56305=CARTESIAN_POINT('Ctrl Pts',(-0.341834277323639,0.235206080702865,
0.563127353040474));
#56306=CARTESIAN_POINT('Ctrl Pts',(-0.378249882633598,0.110101262730849,
0.569748487495545));
#56307=CARTESIAN_POINT('Ctrl Pts',(-0.388580829934269,0.0746095752927858,
0.57162687426253));
#56308=CARTESIAN_POINT('Ctrl Pts',(-0.393421317183489,0.0375197205815717,
0.573505261029516));
#56309=CARTESIAN_POINT('Ctrl Pts',(-0.393104204086639,0.000348908879909379,
0.575383647796501));
#56310=CARTESIAN_POINT('Origin',(0.,0.,0.93));
#56311=CARTESIAN_POINT('',(-0.392696669456933,-0.000135344718680625,0.718716352203497));
#56312=CARTESIAN_POINT('',(-0.392715395849333,-0.000160388007437934,0.700383647796502));
#56313=CARTESIAN_POINT('',(-0.3933,-4.81653586104654E-17,0.93));
#56314=CARTESIAN_POINT('Ctrl Pts',(-0.392696669456933,-0.000135344718680625,
0.718716352203497));
#56315=CARTESIAN_POINT('Ctrl Pts',(-0.392468153843407,0.0739588116703239,
0.714981839773422));
#56316=CARTESIAN_POINT('Ctrl Pts',(-0.37234718500379,0.148168078169027,
0.711247327343347));
#56317=CARTESIAN_POINT('Ctrl Pts',(-0.333113602562395,0.210310632800857,
0.707512814913271));
#56318=CARTESIAN_POINT('Ctrl Pts',(-0.263554100656184,0.32048678492325,
0.7008916804582));
#56319=CARTESIAN_POINT('Ctrl Pts',(-0.133916376170864,0.392732666678619,
0.694270546003128));
#56320=CARTESIAN_POINT('Ctrl Pts',(-0.00362488990349993,0.393931586261435,
0.687649411548057));
#56321=CARTESIAN_POINT('Ctrl Pts',(0.126666596363864,0.395130505844251,
0.681028277092986));
#56322=CARTESIAN_POINT('Ctrl Pts',(0.257611844413273,0.325282463254515,
0.674407142637916));
#56323=CARTESIAN_POINT('Ctrl Pts',(0.32918703949367,0.216405008053231,0.667786008182845));
#56324=CARTESIAN_POINT('Ctrl Pts',(0.400762234574067,0.107527552851948,
0.661164873727774));
#56325=CARTESIAN_POINT('Ctrl Pts',(0.412967376685453,-0.0403793149608816,
0.654543739272702));
#56326=CARTESIAN_POINT('Ctrl Pts',(0.360207767279832,-0.159516766743925,
0.647922604817631));
#56327=CARTESIAN_POINT('Ctrl Pts',(0.307448157874211,-0.278654218526967,
0.641301470362559));
#56328=CARTESIAN_POINT('Ctrl Pts',(0.189723796951584,-0.369022254280223,
0.634680335907489));
#56329=CARTESIAN_POINT('Ctrl Pts',(0.0609981947349131,-0.38919719259095,
0.628059201452418));
#56330=CARTESIAN_POINT('Ctrl Pts',(-0.0677274074817583,-0.409372130901677,
0.621438066997347));
#56331=CARTESIAN_POINT('Ctrl Pts',(-0.207454250992473,-0.359353971769874,
0.614816932542275));
#56332=CARTESIAN_POINT('Ctrl Pts',(-0.294133137407089,-0.26207047136149,
0.608195798087204));
#56333=CARTESIAN_POINT('Ctrl Pts',(-0.35731779020926,-0.191155575578438,
0.603369316125968));
#56334=CARTESIAN_POINT('Ctrl Pts',(-0.392314380621845,-0.0951253226411819,
0.598542834164733));
#56335=CARTESIAN_POINT('Ctrl Pts',(-0.393151626951805,0.000355166996054868,
0.593716352203497));
#56336=CARTESIAN_POINT('Ctrl Pts',(-0.393104204086639,0.000348908879909379,
0.575383647796501));
#56337=CARTESIAN_POINT('Ctrl Pts',(-0.392303523719111,-0.0935038504989454,
0.580126395484587));
#56338=CARTESIAN_POINT('Ctrl Pts',(-0.35862239822199,-0.187872722353307,
0.584869143172672));
#56339=CARTESIAN_POINT('Ctrl Pts',(-0.297418747627281,-0.258335731793845,
0.589611890860758));
#56340=CARTESIAN_POINT('Ctrl Pts',(-0.211975113181625,-0.356705936219178,
0.596233025315829));
#56341=CARTESIAN_POINT('Ctrl Pts',(-0.0728909501609335,-0.408484372942498,
0.602854159770901));
#56342=CARTESIAN_POINT('Ctrl Pts',(0.0560791404910008,-0.389936394519486,
0.609475294225972));
#56343=CARTESIAN_POINT('Ctrl Pts',(0.185049231142934,-0.371388416096473,
0.616096428681043));
#56344=CARTESIAN_POINT('Ctrl Pts',(0.303905249426109,-0.282514022527131,
0.622717563136114));
#56345=CARTESIAN_POINT('Ctrl Pts',(0.358164946230055,-0.164052226618296,
0.629338697591185));
#56346=CARTESIAN_POINT('Ctrl Pts',(0.412424643034,-0.0455904307094625,0.635959832046256));
#56347=CARTESIAN_POINT('Ctrl Pts',(0.402088018358715,0.102458767538864,
0.642580966501327));
#56348=CARTESIAN_POINT('Ctrl Pts',(0.331893263579618,0.212231296835213,
0.649202100956398));
#56349=CARTESIAN_POINT('Ctrl Pts',(0.261698508800521,0.322003826131562,
0.655823235411469));
#56350=CARTESIAN_POINT('Ctrl Pts',(0.131645623917614,0.393499686475935,
0.66244436986654));
#56351=CARTESIAN_POINT('Ctrl Pts',(0.00134937453860157,0.393945987357729,
0.669065504321611));
#56352=CARTESIAN_POINT('Ctrl Pts',(-0.12894687484041,0.394392288239522,
0.675686638776682));
#56353=CARTESIAN_POINT('Ctrl Pts',(-0.259486488715526,0.323789029658737,
0.682307773231754));
#56354=CARTESIAN_POINT('Ctrl Pts',(-0.330431590434274,0.214499943611983,
0.688928907686825));
#56355=CARTESIAN_POINT('Ctrl Pts',(-0.37134389973501,0.1514755940344,0.692747154390051));
#56356=CARTESIAN_POINT('Ctrl Pts',(-0.392437770891352,0.0755860887410146,
0.696565401093276));
#56357=CARTESIAN_POINT('Ctrl Pts',(-0.392715395849333,-0.000160388007437934,
0.700383647796502));
#56358=CARTESIAN_POINT('Origin',(0.,0.,0.93));
#56359=CARTESIAN_POINT('',(-0.393648583493532,-0.000293579281448297,0.843716352203497));
#56360=CARTESIAN_POINT('',(-0.393692585105431,-0.000275383461774757,0.825383647796502));
#56361=CARTESIAN_POINT('',(-0.3933,-4.81653586104654E-17,0.93));
#56362=CARTESIAN_POINT('Ctrl Pts',(-0.393648583493532,-0.000293579281448297,
0.843716352203497));
#56363=CARTESIAN_POINT('Ctrl Pts',(-0.392716383215227,0.111596578592595,
0.838041979837182));
#56364=CARTESIAN_POINT('Ctrl Pts',(-0.342624531659322,0.22421618264734,
0.832367607470866));
#56365=CARTESIAN_POINT('Ctrl Pts',(-0.258315374189583,0.297436383010721,
0.826693235104551));
#56366=CARTESIAN_POINT('Ctrl Pts',(-0.159939336918106,0.382873284246015,
0.820072100649479));
#56367=CARTESIAN_POINT('Ctrl Pts',(-0.0149752034932887,0.414666476295674,
0.813450966194408));
#56368=CARTESIAN_POINT('Ctrl Pts',(0.110127113469719,0.378242320953161,
0.806829831739337));
#56369=CARTESIAN_POINT('Ctrl Pts',(0.235229430432725,0.341818165610649,
0.800208697284266));
#56370=CARTESIAN_POINT('Ctrl Pts',(0.340469930933922,0.237176662875967,
0.793587562829195));
#56371=CARTESIAN_POINT('Ctrl Pts',(0.377607564606836,0.112284289341377,
0.786966428374124));
#56372=CARTESIAN_POINT('Ctrl Pts',(0.414745198279751,-0.0126080841932143,
0.780345293919053));
#56373=CARTESIAN_POINT('Ctrl Pts',(0.383779965124383,-0.157751328527715,
0.773724159463982));
#56374=CARTESIAN_POINT('Ctrl Pts',(0.29890597639204,-0.256613428639898,
0.767103025008911));
#56375=CARTESIAN_POINT('Ctrl Pts',(0.214031987659696,-0.355475528752083,
0.760481890553839));
#56376=CARTESIAN_POINT('Ctrl Pts',(0.0752492433503761,-0.408056484641949,
0.753860756098768));
#56377=CARTESIAN_POINT('Ctrl Pts',(-0.0538258224982624,-0.390253783214973,
0.747239621643697));
#56378=CARTESIAN_POINT('Ctrl Pts',(-0.182900888346899,-0.372451081787997,
0.740618487188626));
#56379=CARTESIAN_POINT('Ctrl Pts',(-0.302268275734855,-0.284264723044181,
0.733997352733555));
#56380=CARTESIAN_POINT('Ctrl Pts',(-0.357211329765281,-0.166118332427566,
0.727376218278484));
#56381=CARTESIAN_POINT('Ctrl Pts',(-0.381164903123588,-0.114609942794055,
0.724489596253488));
#56382=CARTESIAN_POINT('Ctrl Pts',(-0.392873302475408,-0.0574070308519249,
0.721602974228493));
#56383=CARTESIAN_POINT('Ctrl Pts',(-0.392696669456933,-0.000135344718680625,
0.718716352203497));
#56384=CARTESIAN_POINT('Ctrl Pts',(-0.392715395849333,-0.000160388007437934,
0.700383647796502));
#56385=CARTESIAN_POINT('Ctrl Pts',(-0.392919193994087,-0.0557641476451545,
0.703186535548347));
#56386=CARTESIAN_POINT('Ctrl Pts',(-0.381905756157218,-0.11129083359123,
0.705989423300192));
#56387=CARTESIAN_POINT('Ctrl Pts',(-0.359280377758478,-0.161594776908665,
0.708792311052037));
#56388=CARTESIAN_POINT('Ctrl Pts',(-0.305833473801554,-0.28042549786984,
0.715413445507108));
#56389=CARTESIAN_POINT('Ctrl Pts',(-0.187589076325322,-0.370112026279464,
0.72203457996218));
#56390=CARTESIAN_POINT('Ctrl Pts',(-0.0587490744031055,-0.389543075953546,
0.728655714417251));
#56391=CARTESIAN_POINT('Ctrl Pts',(0.0700909275191088,-0.408974125627628,
0.735276848872322));
#56392=CARTESIAN_POINT('Ctrl Pts',(0.209526533887308,-0.35814969656617,
0.741897983327393));
#56393=CARTESIAN_POINT('Ctrl Pts',(0.295642046109568,-0.260367129912076,
0.748519117782464));
#56394=CARTESIAN_POINT('Ctrl Pts',(0.381757558331829,-0.162584563257981,
0.755140252237535));
#56395=CARTESIAN_POINT('Ctrl Pts',(0.414552976408151,-0.0178438590112496,
0.761761386692606));
#56396=CARTESIAN_POINT('Ctrl Pts',(0.378995253102251,0.107507487611169,
0.768382521147677));
#56397=CARTESIAN_POINT('Ctrl Pts',(0.343437529796352,0.232858834233588,
0.775003655602749));
#56398=CARTESIAN_POINT('Ctrl Pts',(0.239526665108231,0.338820823231692,
0.78162479005782));
#56399=CARTESIAN_POINT('Ctrl Pts',(0.114894219446364,0.376821682104857,
0.788245924512891));
#56400=CARTESIAN_POINT('Ctrl Pts',(-0.00973822621550149,0.414822540978021,
0.794867058967962));
#56401=CARTESIAN_POINT('Ctrl Pts',(-0.155092252851112,0.384862269726245,
0.801488193423032));
#56402=CARTESIAN_POINT('Ctrl Pts',(-0.254539225224928,0.30067431647616,
0.808109327878103));
#56403=CARTESIAN_POINT('Ctrl Pts',(-0.341023841386423,0.227459791705242,
0.813867434517569));
#56404=CARTESIAN_POINT('Ctrl Pts',(-0.392788913023703,0.113232824514289,
0.819625541157036));
#56405=CARTESIAN_POINT('Ctrl Pts',(-0.393692585105431,-0.000275383461774757,
0.825383647796502));
#56406=CARTESIAN_POINT('Origin',(0.,0.,0.93));
#56407=CARTESIAN_POINT('',(-0.393623414358295,0.000302776322228852,0.968716352203497));
#56408=CARTESIAN_POINT('',(-0.393576675000574,0.000317769076113512,0.950383647796502));
#56409=CARTESIAN_POINT('',(-0.3933,-4.81653586104654E-17,0.93));
#56410=CARTESIAN_POINT('Ctrl Pts',(-0.393623414358295,0.000302776322228852,
0.968716352203497));
#56411=CARTESIAN_POINT('Ctrl Pts',(-0.393790054855682,0.0198884434456063,
0.967723254356012));
#56412=CARTESIAN_POINT('Ctrl Pts',(-0.392454790325599,0.0394513098675264,
0.966730156508528));
#56413=CARTESIAN_POINT('Ctrl Pts',(-0.389539024169359,0.0587757018706559,
0.965737058661043));
#56414=CARTESIAN_POINT('Ctrl Pts',(-0.370099167554116,0.187614363679551,
0.959115924205972));
#56415=CARTESIAN_POINT('Ctrl Pts',(-0.280404562957203,0.305852618684086,
0.952494789750901));
#56416=CARTESIAN_POINT('Ctrl Pts',(-0.161570198594696,0.359291393450046,
0.94587365529583));
#56417=CARTESIAN_POINT('Ctrl Pts',(-0.0427358342321878,0.412730168216006,
0.939252520840759));
#56418=CARTESIAN_POINT('Ctrl Pts',(0.105238289895915,0.401369462743389,
0.932631386385688));
#56419=CARTESIAN_POINT('Ctrl Pts',(0.214522515616161,0.330416895413838,
0.926010251930617));
#56420=CARTESIAN_POINT('Ctrl Pts',(0.323806741336407,0.259464328084287,
0.919389117475546));
#56421=CARTESIAN_POINT('Ctrl Pts',(0.394401068648798,0.128919898897802,
0.912767983020475));
#56422=CARTESIAN_POINT('Ctrl Pts',(0.393945859550417,-0.00137630820971424,
0.906146848565404));
#56423=CARTESIAN_POINT('Ctrl Pts',(0.393490650452036,-0.131672515317231,
0.899525714110333));
#56424=CARTESIAN_POINT('Ctrl Pts',(0.321985904942885,-0.261720500345779,
0.892904579655261));
#56425=CARTESIAN_POINT('Ctrl Pts',(0.212208586388978,-0.331907743724061,
0.88628344520019));
#56426=CARTESIAN_POINT('Ctrl Pts',(0.102431267835071,-0.402094987102343,
0.879662310745119));
#56427=CARTESIAN_POINT('Ctrl Pts',(-0.0456186237635904,-0.412421488830358,
0.873041176290049));
#56428=CARTESIAN_POINT('Ctrl Pts',(-0.164076699285435,-0.358153697779043,
0.866420041834977));
#56429=CARTESIAN_POINT('Ctrl Pts',(-0.282534774807279,-0.303885906727728,
0.859798907379906));
#56430=CARTESIAN_POINT('Ctrl Pts',(-0.371401034252306,-0.185023822897081,
0.853177772924835));
#56431=CARTESIAN_POINT('Ctrl Pts',(-0.389940193415752,-0.056052475771292,
0.846556638469764));
#56432=CARTESIAN_POINT('Ctrl Pts',(-0.392591124788987,-0.0376107445509109,
0.845609876381008));
#56433=CARTESIAN_POINT('Ctrl Pts',(-0.393804119969754,-0.0189623152651601,
0.844663114292253));
#56434=CARTESIAN_POINT('Ctrl Pts',(-0.393648583493532,-0.000293579281448297,
0.843716352203497));
#56435=CARTESIAN_POINT('Ctrl Pts',(-0.393692585105431,-0.000275383461774757,
0.825383647796502));
#56436=CARTESIAN_POINT('Ctrl Pts',(-0.39382802791529,-0.0172880487207719,
0.826246675612107));
#56437=CARTESIAN_POINT('Ctrl Pts',(-0.392820912119232,-0.034284567657927,
0.827109703427712));
#56438=CARTESIAN_POINT('Ctrl Pts',(-0.390616889073419,-0.0511244338562125,
0.827972731243317));
#56439=CARTESIAN_POINT('Ctrl Pts',(-0.373707662436067,-0.180319595690092,
0.834593865698388));
#56440=CARTESIAN_POINT('Ctrl Pts',(-0.286349291049343,-0.300294284109454,
0.841215000153459));
#56441=CARTESIAN_POINT('Ctrl Pts',(-0.168585860354973,-0.356053464320865,
0.84783613460853));
#56442=CARTESIAN_POINT('Ctrl Pts',(-0.0508224296606021,-0.411812644532276,
0.854457269063601));
#56443=CARTESIAN_POINT('Ctrl Pts',(0.0973460603414153,-0.403356316535735,
0.861078403518672));
#56444=CARTESIAN_POINT('Ctrl Pts',(0.208000856368157,-0.334560765058647,
0.867699537973743));
#56445=CARTESIAN_POINT('Ctrl Pts',(0.318655652394899,-0.265765213581559,
0.874320672428815));
#56446=CARTESIAN_POINT('Ctrl Pts',(0.391796754446365,-0.136630438623923,
0.880941806883886));
#56447=CARTESIAN_POINT('Ctrl Pts',(0.393897111899264,-0.00635035463052729,
0.887562941338957));
#56448=CARTESIAN_POINT('Ctrl Pts',(0.395997469352162,0.123929729362869,
0.894184075794028));
#56449=CARTESIAN_POINT('Ctrl Pts',(0.327057082206493,0.255355122392025,
0.900805210249099));
#56450=CARTESIAN_POINT('Ctrl Pts',(0.21867744107414,0.327681916699382,0.90742634470417));
#56451=CARTESIAN_POINT('Ctrl Pts',(0.110297799941786,0.40000871100674,0.914047479159241));
#56452=CARTESIAN_POINT('Ctrl Pts',(-0.0375210951772516,0.413236906592297,
0.920668613614312));
#56453=CARTESIAN_POINT('Ctrl Pts',(-0.157020741324571,0.36130284881301,
0.927289748069384));
#56454=CARTESIAN_POINT('Ctrl Pts',(-0.276520387471888,0.309368791033724,
0.933910882524455));
#56455=CARTESIAN_POINT('Ctrl Pts',(-0.367700784647487,0.192272479889591,
0.940532016979525));
#56456=CARTESIAN_POINT('Ctrl Pts',(-0.388765874189203,0.0636895347166177,
0.947153151434597));
#56457=CARTESIAN_POINT('Ctrl Pts',(-0.392191807493608,0.0427773713301666,
0.948229983555232));
#56458=CARTESIAN_POINT('Ctrl Pts',(-0.39376316737147,0.0215613826172752,
0.949306815675866));
#56459=CARTESIAN_POINT('Ctrl Pts',(-0.393576675000574,0.000317769076113512,
0.950383647796502));
#56460=CARTESIAN_POINT('Origin',(0.,0.,0.93));
#56461=CARTESIAN_POINT('',(-0.392687717376401,0.000121152120971441,1.0937163522035));
#56462=CARTESIAN_POINT('',(-0.392674134765212,9.49958190125592E-5,1.0753836477965));
#56463=CARTESIAN_POINT('',(-0.3933,-4.81653586104654E-17,0.93));
#56464=CARTESIAN_POINT('Ctrl Pts',(-0.392687717376401,0.000121152120971441,
1.0937163522035));
#56465=CARTESIAN_POINT('Ctrl Pts',(-0.392848158650017,0.0583154695936899,
1.09078339441977));
#56466=CARTESIAN_POINT('Ctrl Pts',(-0.380745062692883,0.116446324066143,
1.08785043663605));
#56467=CARTESIAN_POINT('Ctrl Pts',(-0.356041906099905,0.168610188250716,
1.08491747885232));
#56468=CARTESIAN_POINT('Ctrl Pts',(-0.300274679522556,0.286369796104153,
1.07829634439725));
#56469=CARTESIAN_POINT('Ctrl Pts',(-0.180294029303511,0.373719957027504,
1.07167520994218));
#56470=CARTESIAN_POINT('Ctrl Pts',(-0.051097723057459,0.390620349162146,
1.06505407548711));
#56471=CARTESIAN_POINT('Ctrl Pts',(0.0780985831885896,0.407520741296788,
1.05843294103204));
#56472=CARTESIAN_POINT('Ctrl Pts',(0.216510545461646,0.353971364642725,
1.05181180657697));
#56473=CARTESIAN_POINT('Ctrl Pts',(0.300691691999046,0.254518645375842,
1.0451906721219));
#56474=CARTESIAN_POINT('Ctrl Pts',(0.384872838536448,0.155065926108957,
1.03856953766683));
#56475=CARTESIAN_POINT('Ctrl Pts',(0.414823169338192,0.00970986422925148,
1.03194840321175));
#56476=CARTESIAN_POINT('Ctrl Pts',(0.376813792867102,-0.114919972094987,
1.02532726875668));
#56477=CARTESIAN_POINT('Ctrl Pts',(0.338804416396012,-0.239549808419227,
1.01870613430161));
#56478=CARTESIAN_POINT('Ctrl Pts',(0.232835332652085,-0.343453419187998,
1.01208499984654));
#56479=CARTESIAN_POINT('Ctrl Pts',(0.107481566286803,-0.379002569107047,
1.00546386539147));
#56480=CARTESIAN_POINT('Ctrl Pts',(-0.0178722000784767,-0.414551719026095,
0.998842730936399));
#56481=CARTESIAN_POINT('Ctrl Pts',(-0.162610649065111,-0.381746408095422,
0.992221596481328));
#56482=CARTESIAN_POINT('Ctrl Pts',(-0.260387319241642,-0.295624218323459,
0.985600462026257));
#56483=CARTESIAN_POINT('Ctrl Pts',(-0.343498556878564,-0.222419416329008,
0.97997242541867));
#56484=CARTESIAN_POINT('Ctrl Pts',(-0.392679037304232,-0.110692179344585,
0.974344388811084));
#56485=CARTESIAN_POINT('Ctrl Pts',(-0.393623414358295,0.000302776322228852,
0.968716352203497));
#56486=CARTESIAN_POINT('Ctrl Pts',(-0.393576675000574,0.000317769076113512,
0.950383647796502));
#56487=CARTESIAN_POINT('Ctrl Pts',(-0.392616478821894,-0.109059555291462,
0.955927950130938));
#56488=CARTESIAN_POINT('Ctrl Pts',(-0.345056898727053,-0.219169193753748,
0.961472252465374));
#56489=CARTESIAN_POINT('Ctrl Pts',(-0.264099282894184,-0.292312898349171,
0.96701655479981));
#56490=CARTESIAN_POINT('Ctrl Pts',(-0.167417820149611,-0.379662807040174,
0.973637689254881));
#56491=CARTESIAN_POINT('Ctrl Pts',(-0.0231051127526314,-0.414293045220361,
0.980258823709952));
#56492=CARTESIAN_POINT('Ctrl Pts',(0.102687532975472,-0.380329504953174,
0.986879958165023));
#56493=CARTESIAN_POINT('Ctrl Pts',(0.228480178703574,-0.346365964685987,
0.993501092620094));
#56494=CARTESIAN_POINT('Ctrl Pts',(0.335752762762798,-0.243808645971423,
1.00012222707516));
#56495=CARTESIAN_POINT('Ctrl Pts',(0.375332750759084,-0.119668659113963,
1.00674336153024));
#56496=CARTESIAN_POINT('Ctrl Pts',(0.414912738755369,0.00447132774349662,
1.01336449598531));
#56497=CARTESIAN_POINT('Ctrl Pts',(0.386800130688718,0.150193982743854,
1.01998563044038));
#56498=CARTESIAN_POINT('Ctrl Pts',(0.303881426862889,0.250701695595161,
1.02660676489545));
#56499=CARTESIAN_POINT('Ctrl Pts',(0.22096272303706,0.351209408446469,1.03322789935052));
#56500=CARTESIAN_POINT('Ctrl Pts',(0.0832379234520517,0.406502179148727,
1.03984903380559));
#56501=CARTESIAN_POINT('Ctrl Pts',(-0.0461614877025709,0.391234429491579,
1.04647016826066));
#56502=CARTESIAN_POINT('Ctrl Pts',(-0.175560898857193,0.375966679834431,
1.05309130271573));
#56503=CARTESIAN_POINT('Ctrl Pts',(-0.296634921581431,0.290138409817877,
1.0597124371708));
#56504=CARTESIAN_POINT('Ctrl Pts',(-0.353884598720045,0.173092323790705,
1.06633357162588));
#56505=CARTESIAN_POINT('Ctrl Pts',(-0.379968443936397,0.119764302678541,
1.06935026368275));
#56506=CARTESIAN_POINT('Ctrl Pts',(-0.392803276473094,0.059955913669758,
1.07236695573963));
#56507=CARTESIAN_POINT('Ctrl Pts',(-0.392674134765212,9.49958190125592E-5,
1.0753836477965));
#56508=CARTESIAN_POINT('Origin',(0.,0.,0.93));
#56509=CARTESIAN_POINT('',(-0.393178387374057,-0.000357709694404185,1.2187163522035));
#56510=CARTESIAN_POINT('',(-0.393227518215404,-0.000360608651032692,1.2003836477965));
#56511=CARTESIAN_POINT('',(-0.3933,-4.81653586104654E-17,0.93));
#56512=CARTESIAN_POINT('Ctrl Pts',(-0.393178387374057,-0.000357709694404185,
1.2187163522035));
#56513=CARTESIAN_POINT('Ctrl Pts',(-0.392322385109892,0.0960227493030975,
1.21384353448353));
#56514=CARTESIAN_POINT('Ctrl Pts',(-0.356584758291295,0.192971013585422,
1.20897071676357));
#56515=CARTESIAN_POINT('Ctrl Pts',(-0.292294815698811,0.264119244274569,
1.2040978990436));
#56516=CARTESIAN_POINT('Ctrl Pts',(-0.204938304850977,0.360794726245326,
1.19747676458853));
#56517=CARTESIAN_POINT('Ctrl Pts',(-0.0648653847631109,0.409835363460394,
1.19085563013346));
#56518=CARTESIAN_POINT('Ctrl Pts',(0.0637161086015447,0.388761484700158,
1.18423449567839));
#56519=CARTESIAN_POINT('Ctrl Pts',(0.192297601966202,0.367687605939922,
1.17761336122332));
#56520=CARTESIAN_POINT('Ctrl Pts',(0.309387668607649,0.27649921120438,1.17099222676825));
#56521=CARTESIAN_POINT('Ctrl Pts',(0.361313551598668,0.156996025148134,
1.16437109231318));
#56522=CARTESIAN_POINT('Ctrl Pts',(0.413239434589687,0.037492839091888,
1.1577499578581));
#56523=CARTESIAN_POINT('Ctrl Pts',(0.400001133930281,-0.11032513828506,
1.15112882340303));
#56524=CARTESIAN_POINT('Ctrl Pts',(0.327666936314771,-0.218699824707789,
1.14450768894796));
#56525=CARTESIAN_POINT('Ctrl Pts',(0.255332738699263,-0.327074511130518,
1.13788655449289));
#56526=CARTESIAN_POINT('Ctrl Pts',(0.123902644127651,-0.396005906599026,
1.13126542003782));
#56527=CARTESIAN_POINT('Ctrl Pts',(-0.00637728450892158,-0.393896642183651,
1.12464428558275));
#56528=CARTESIAN_POINT('Ctrl Pts',(-0.136657213145495,-0.391787377768276,
1.11802315112768));
#56529=CARTESIAN_POINT('Ctrl Pts',(-0.26578697584703,-0.318637453469018,
1.11140201667261));
#56530=CARTESIAN_POINT('Ctrl Pts',(-0.33457495572997,-0.207977963927629,
1.10478088221754));
#56531=CARTESIAN_POINT('Ctrl Pts',(-0.372891988014216,-0.146337205752564,
1.10109270554619));
#56532=CARTESIAN_POINT('Ctrl Pts',(-0.392485963445352,-0.0730578500790584,
1.09740452887484));
#56533=CARTESIAN_POINT('Ctrl Pts',(-0.392687717376401,0.000121152120971441,
1.0937163522035));
#56534=CARTESIAN_POINT('Ctrl Pts',(-0.392674134765212,9.49958190125592E-5,
1.0753836477965));
#56535=CARTESIAN_POINT('Ctrl Pts',(-0.392519832026156,-0.0714287879243111,
1.0789880901947));
#56536=CARTESIAN_POINT('Ctrl Pts',(-0.373857832359423,-0.143027563168594,
1.08259253259289));
#56537=CARTESIAN_POINT('Ctrl Pts',(-0.337174346736183,-0.203736893246021,
1.08619697499109));
#56538=CARTESIAN_POINT('Ctrl Pts',(-0.269789086060714,-0.315256122217786,
1.09281810944616));
#56539=CARTESIAN_POINT('Ctrl Pts',(-0.141593233156782,-0.390030678123524,
1.09943924390123));
#56540=CARTESIAN_POINT('Ctrl Pts',(-0.0113503112617354,-0.393784753641865,
1.1060603783563));
#56541=CARTESIAN_POINT('Ctrl Pts',(0.11889261063331,-0.397538829160207,
1.11268151281137));
#56542=CARTESIAN_POINT('Ctrl Pts',(0.25118260151947,-0.330272424291154,
1.11930264726645));
#56543=CARTESIAN_POINT('Ctrl Pts',(0.32487943179952,-0.222819695180042,
1.12592378172152));
#56544=CARTESIAN_POINT('Ctrl Pts',(0.398576262079569,-0.115366966068929,
1.13254491617659));
#56545=CARTESIAN_POINT('Ctrl Pts',(0.413679931753507,0.0322720872842442,
1.13916605063166));
#56546=CARTESIAN_POINT('Ctrl Pts',(0.363267090153202,0.152421399344478,
1.14578718508673));
#56547=CARTESIAN_POINT('Ctrl Pts',(0.312854248552898,0.272570711404711,
1.1524083195418));
#56548=CARTESIAN_POINT('Ctrl Pts',(0.196924895678351,0.365230282172005,
1.15902945399687));
#56549=CARTESIAN_POINT('Ctrl Pts',(0.0686197304462398,0.387926016606333,
1.16565058845194));
#56550=CARTESIAN_POINT('Ctrl Pts',(-0.0596854347858714,0.410621751040662,
1.17227172290701));
#56551=CARTESIAN_POINT('Ctrl Pts',(-0.200366412375547,0.363353649142024,
1.17889285736209));
#56552=CARTESIAN_POINT('Ctrl Pts',(-0.28893663970491,0.26778887206617,1.18551399181716));
#56553=CARTESIAN_POINT('Ctrl Pts',(-0.355239920476351,0.196249502264644,
1.19047054381027));
#56554=CARTESIAN_POINT('Ctrl Pts',(-0.392340579448797,0.0976449005809497,
1.19542709580339));
#56555=CARTESIAN_POINT('Ctrl Pts',(-0.393227518215404,-0.000360608651032693,
1.2003836477965));
#56556=CARTESIAN_POINT('Origin',(0.,0.,0.93));
#56557=CARTESIAN_POINT('',(-0.393932958190319,7.01566447607431E-5,1.3437163522035));
#56558=CARTESIAN_POINT('',(-0.393917393671661,0.000100014571609002,1.3253836477965));
#56559=CARTESIAN_POINT('',(-0.3933,-4.81653586104654E-17,0.93));
#56560=CARTESIAN_POINT('Ctrl Pts',(-0.393932958190319,7.01566447607431E-5,
1.3437163522035));
#56561=CARTESIAN_POINT('Ctrl Pts',(-0.393942224805097,0.00383992058097464,
1.34352480900236));
#56562=CARTESIAN_POINT('Ctrl Pts',(-0.393892801581458,0.00760943545943395,
1.34333326580123));
#56563=CARTESIAN_POINT('Ctrl Pts',(-0.393783942110804,0.0113772331014927,
1.3431417226001));
#56564=CARTESIAN_POINT('Ctrl Pts',(-0.390020962335796,0.141619886663971,
1.33652058814502));
#56565=CARTESIAN_POINT('Ctrl Pts',(-0.31523764848855,0.269810615534473,
1.32989945368995));
#56566=CARTESIAN_POINT('Ctrl Pts',(-0.20371382249242,0.337188245598414,
1.32327831923488));
#56567=CARTESIAN_POINT('Ctrl Pts',(-0.0921899964962896,0.404565875662355,
1.31665718477981));
#56568=CARTESIAN_POINT('Ctrl Pts',(0.0560743416487236,0.411130406919734,
1.31003605032474));
#56569=CARTESIAN_POINT('Ctrl Pts',(0.173116502991226,0.353872732616968,
1.30341491586967));
#56570=CARTESIAN_POINT('Ctrl Pts',(0.290158664333728,0.296615058314203,
1.2967937814146));
#56571=CARTESIAN_POINT('Ctrl Pts',(0.375978648873719,0.175535178451293,
1.29017264695953));
#56572=CARTESIAN_POINT('Ctrl Pts',(0.391237550214167,0.0461347351175119,
1.28355151250445));
#56573=CARTESIAN_POINT('Ctrl Pts',(0.406496451554614,-0.0832657082162682,
1.27693037804938));
#56574=CARTESIAN_POINT('Ctrl Pts',(0.351194269695518,-0.220986715020921,
1.27030924359431));
#56575=CARTESIAN_POINT('Ctrl Pts',(0.250680896823328,-0.303898539720326,
1.26368810913924));
#56576=CARTESIAN_POINT('Ctrl Pts',(0.150167523951137,-0.386810364419732,
1.25706697468417));
#56577=CARTESIAN_POINT('Ctrl Pts',(0.00444296006585079,-0.414913007013892,
1.2504458402291));
#56578=CARTESIAN_POINT('Ctrl Pts',(-0.119694309533929,-0.375324535234475,
1.24382470577403));
#56579=CARTESIAN_POINT('Ctrl Pts',(-0.243831579133704,-0.335736063455059,
1.23720357131896));
#56580=CARTESIAN_POINT('Ctrl Pts',(-0.346381554447974,-0.228456477302072,
1.23058243686389));
#56581=CARTESIAN_POINT('Ctrl Pts',(-0.38033649130121,-0.102661520862356,
1.22396130240882));
#56582=CARTESIAN_POINT('Ctrl Pts',(-0.389302324081501,-0.0694452451579606,
1.22221298567371));
#56583=CARTESIAN_POINT('Ctrl Pts',(-0.393485512156828,-0.0349380242241585,
1.2204646689386));
#56584=CARTESIAN_POINT('Ctrl Pts',(-0.393178387374057,-0.000357709694404185,
1.2187163522035));
#56585=CARTESIAN_POINT('Ctrl Pts',(-0.393227518215404,-0.000360608651032693,
1.2003836477965));
#56586=CARTESIAN_POINT('Ctrl Pts',(-0.393525383085535,-0.0332742655781063,
1.20204823025846));
#56587=CARTESIAN_POINT('Ctrl Pts',(-0.389738883964958,-0.0661203538703375,
1.20371281272041));
#56588=CARTESIAN_POINT('Ctrl Pts',(-0.381602460640826,-0.0978510286064153,
1.20537739518237));
#56589=CARTESIAN_POINT('Ctrl Pts',(-0.349238577178329,-0.22406469995007,
1.21199852963744));
#56590=CARTESIAN_POINT('Ctrl Pts',(-0.248051333184284,-0.332630590384309,
1.21861966409251));
#56591=CARTESIAN_POINT('Ctrl Pts',(-0.124423812269278,-0.373783328557174,
1.22524079854758));
#56592=CARTESIAN_POINT('Ctrl Pts',(-0.000796291354272574,-0.414936066730039,
1.23186193300265));
#56593=CARTESIAN_POINT('Ctrl Pts',(0.145271506481696,-0.388675652641532,
1.23848306745772));
#56594=CARTESIAN_POINT('Ctrl Pts',(0.246823761390213,-0.307039561911936,
1.2451042019128));
#56595=CARTESIAN_POINT('Ctrl Pts',(0.348376016298731,-0.225403471182339,
1.25172533636787));
#56596=CARTESIAN_POINT('Ctrl Pts',(0.405412728279798,-0.0883917038116555,
1.25834647082294));
#56597=CARTESIAN_POINT('Ctrl Pts',(0.391788916244076,0.0411911018873178,
1.26496760527801));
#56598=CARTESIAN_POINT('Ctrl Pts',(0.378165104208354,0.17077390758629,1.27158873973308));
#56599=CARTESIAN_POINT('Ctrl Pts',(0.293880768155842,0.292927751613551,
1.27820987418815));
#56600=CARTESIAN_POINT('Ctrl Pts',(0.177570890638771,0.351658698977885,
1.28483100864322));
#56601=CARTESIAN_POINT('Ctrl Pts',(0.0612610131216984,0.41038964634222,
1.29145214309829));
#56602=CARTESIAN_POINT('Ctrl Pts',(-0.0870744058599348,0.405697697043627,
1.29807327755336));
#56603=CARTESIAN_POINT('Ctrl Pts',(-0.199440094675204,0.339733587385156,
1.30469441200844));
#56604=CARTESIAN_POINT('Ctrl Pts',(-0.311805783490471,0.273769477726686,
1.31131554646351));
#56605=CARTESIAN_POINT('Ctrl Pts',(-0.388201742139376,0.14653320770834,
1.31793668091858));
#56606=CARTESIAN_POINT('Ctrl Pts',(-0.393608930693719,0.0163484386228601,
1.32455781537365));
#56607=CARTESIAN_POINT('Ctrl Pts',(-0.393833737668765,0.010935931949371,
1.32483309284793));
#56608=CARTESIAN_POINT('Ctrl Pts',(-0.393935838534097,0.00551832871131889,
1.32510837032222));
#56609=CARTESIAN_POINT('Ctrl Pts',(-0.393917393671661,0.000100014571609002,
1.3253836477965));
#56610=CARTESIAN_POINT('Origin',(0.,0.,0.93));
#56611=CARTESIAN_POINT('',(-0.392969983056837,0.000317581071747716,1.4687163522035));
#56612=CARTESIAN_POINT('',(-0.39292938619043,0.000303368867518512,1.4503836477965));
#56613=CARTESIAN_POINT('',(-0.3933,-4.81653586104654E-17,0.93));
#56614=CARTESIAN_POINT('Ctrl Pts',(-0.392969983056837,0.000317581071747716,
1.4687163522035));
#56615=CARTESIAN_POINT('Ctrl Pts',(-0.393289547738009,0.0425316776590403,
1.46658494906612));
#56616=CARTESIAN_POINT('Ctrl Pts',(-0.387024947442207,0.0846534505080271,
1.46445354592875));
#56617=CARTESIAN_POINT('Ctrl Pts',(-0.373774788945001,0.124449361011914,
1.46232214279137));
#56618=CARTESIAN_POINT('Ctrl Pts',(-0.332613602953188,0.24807406137376,
1.4557010083363));
#56619=CARTESIAN_POINT('Ctrl Pts',(-0.224040802499859,0.349253864537994,
1.44907987388123));
#56620=CARTESIAN_POINT('Ctrl Pts',(-0.0978249294402324,0.381609113761947,
1.44245873942616));
#56621=CARTESIAN_POINT('Ctrl Pts',(0.0283909436193927,0.4139643629859,1.43583760497109));
#56622=CARTESIAN_POINT('Ctrl Pts',(0.172249889285313,0.377495058269573,
1.42921647051602));
#56623=CARTESIAN_POINT('Ctrl Pts',(0.267808602042126,0.288918306379673,
1.42259533606095));
#56624=CARTESIAN_POINT('Ctrl Pts',(0.363367314798942,0.20034155448977,1.41597420160588));
#56625=CARTESIAN_POINT('Ctrl Pts',(0.410625794646646,0.0596573554262853,
1.40935306715081));
#56626=CARTESIAN_POINT('Ctrl Pts',(0.387921290244053,-0.0686462471308959,
1.40273193269574));
#56627=CARTESIAN_POINT('Ctrl Pts',(0.36521678584146,-0.196949849688075,
1.39611079824066));
#56628=CARTESIAN_POINT('Ctrl Pts',(0.272549297188576,-0.312872855738954,
1.38948966378559));
#56629=CARTESIAN_POINT('Ctrl Pts',(0.152396549224293,-0.36327747796107,
1.38286852933052));
#56630=CARTESIAN_POINT('Ctrl Pts',(0.0322438012600084,-0.413682100183186,
1.37624739487545));
#56631=CARTESIAN_POINT('Ctrl Pts',(-0.115394206015674,-0.398568338576538,
1.36962626042038));
#56632=CARTESIAN_POINT('Ctrl Pts',(-0.222841886802131,-0.324864168645985,
1.36300512596531));
#56633=CARTESIAN_POINT('Ctrl Pts',(-0.327181207099616,-0.253292191127661,
1.35657553471137));
#56634=CARTESIAN_POINT('Ctrl Pts',(-0.393621902799281,-0.126470702493874,
1.35014594345743));
#56635=CARTESIAN_POINT('Ctrl Pts',(-0.393932958190319,7.01566447607431E-5,
1.3437163522035));
#56636=CARTESIAN_POINT('Ctrl Pts',(-0.393917393671661,0.000100014571609002,
1.3253836477965));
#56637=CARTESIAN_POINT('Ctrl Pts',(-0.393492191938935,-0.124806124940763,
1.33172950477729));
#56638=CARTESIAN_POINT('Ctrl Pts',(-0.329006385569408,-0.25009005295616,
1.33807536175808));
#56639=CARTESIAN_POINT('Ctrl Pts',(-0.22692603833899,-0.322024587425646,
1.34442121873886));
#56640=CARTESIAN_POINT('Ctrl Pts',(-0.12041753897014,-0.397079576236056,
1.35104235319393));
#56641=CARTESIAN_POINT('Ctrl Pts',(0.0270178782273391,-0.414056285704261,
1.357663487649));
#56642=CARTESIAN_POINT('Ctrl Pts',(0.147797492224514,-0.365172785160562,
1.36428462210407));
#56643=CARTESIAN_POINT('Ctrl Pts',(0.268577106221691,-0.316289284616863,
1.37090575655915));
#56644=CARTESIAN_POINT('Ctrl Pts',(0.36270091701856,-0.20154557406126,1.37752689101422));
#56645=CARTESIAN_POINT('Ctrl Pts',(0.387023638563781,-0.073538867107662,
1.38414802546929));
#56646=CARTESIAN_POINT('Ctrl Pts',(0.411346360109002,0.0544678398459324,
1.39076915992436));
#56647=CARTESIAN_POINT('Ctrl Pts',(0.365867992402574,0.195737543197524,
1.39739029437943));
#56648=CARTESIAN_POINT('Ctrl Pts',(0.27143530278721,0.285513814497535,1.4040114288345));
#56649=CARTESIAN_POINT('Ctrl Pts',(0.177002613171845,0.375290085797548,
1.41063256328957));
#56650=CARTESIAN_POINT('Ctrl Pts',(0.0336156016475434,0.413572925045984,
1.41725369774464));
#56651=CARTESIAN_POINT('Ctrl Pts',(-0.0929987539746983,0.382813914657498,
1.42387483219972));
#56652=CARTESIAN_POINT('Ctrl Pts',(-0.21961310959694,0.352054904269012,
1.43049596665479));
#56653=CARTESIAN_POINT('Ctrl Pts',(-0.32945480931712,0.252254044243605,
1.43711710110986));
#56654=CARTESIAN_POINT('Ctrl Pts',(-0.372173665230652,0.129158913215852,
1.44373823556493));
#56655=CARTESIAN_POINT('Ctrl Pts',(-0.386465496413208,0.0879767515117977,
1.44595337297545));
#56656=CARTESIAN_POINT('Ctrl Pts',(-0.393244440240979,0.0441873219369639,
1.44816851038598));
#56657=CARTESIAN_POINT('Ctrl Pts',(-0.39292938619043,0.000303368867518512,
1.4503836477965));
#56658=CARTESIAN_POINT('Origin',(0.,0.,0.93));
#56659=CARTESIAN_POINT('',(-0.392790597751209,-0.000230484700094208,1.5937163522035));
#56660=CARTESIAN_POINT('',(-0.392821510739754,-0.000250701325252446,1.5753836477965));
#56661=CARTESIAN_POINT('',(-0.3933,-4.81653586104654E-17,0.93));
#56662=CARTESIAN_POINT('Ctrl Pts',(-0.392790597751209,-0.000230484700094208,
1.5937163522035));
#56663=CARTESIAN_POINT('Ctrl Pts',(-0.392361248393127,0.0804967654600471,
1.58964508912988));
#56664=CARTESIAN_POINT('Ctrl Pts',(-0.368164027480674,0.161460390358751,
1.58557382605627));
#56665=CARTESIAN_POINT('Ctrl Pts',(-0.322009087387059,0.226948266830839,
1.58150256298265));
#56666=CARTESIAN_POINT('Ctrl Pts',(-0.246946862568883,0.333451832790243,
1.57488142852758));
#56667=CARTESIAN_POINT('Ctrl Pts',(-0.113809037324264,0.399023853241257,
1.56826029407251));
#56668=CARTESIAN_POINT('Ctrl Pts',(0.0163753707382398,0.393607656210794,
1.56163915961744));
#56669=CARTESIAN_POINT('Ctrl Pts',(0.146559778800742,0.388191459180332,
1.55501802516237));
#56670=CARTESIAN_POINT('Ctrl Pts',(0.273790769681132,0.311787044668395,
1.5483968907073));
#56671=CARTESIAN_POINT('Ctrl Pts',(0.339747180380717,0.199416912588678,
1.54177575625223));
#56672=CARTESIAN_POINT('Ctrl Pts',(0.405703591080302,0.0870467805089601,
1.53515462179716));
#56673=CARTESIAN_POINT('Ctrl Pts',(0.410385421599083,-0.0612890691385343,
1.52853348734209));
#56674=CARTESIAN_POINT('Ctrl Pts',(0.351646533070016,-0.177594950249301,
1.52191235288702));
#56675=CARTESIAN_POINT('Ctrl Pts',(0.292907644540948,-0.293900831360069,
1.51529121843194));
#56676=CARTESIAN_POINT('Ctrl Pts',(0.170748036964027,-0.378176743934104,
1.50867008397687));
#56677=CARTESIAN_POINT('Ctrl Pts',(0.0411643086114815,-0.391791679881239,
1.5020489495218));
#56678=CARTESIAN_POINT('Ctrl Pts',(-0.0884194197410625,-0.405406615828374,
1.49542781506673));
#56679=CARTESIAN_POINT('Ctrl Pts',(-0.225427268869233,-0.348360575148612,
1.48880668061166));
#56680=CARTESIAN_POINT('Ctrl Pts',(-0.30705640766817,-0.246802756029003,
1.48218554615659));
#56681=CARTESIAN_POINT('Ctrl Pts',(-0.362408387512275,-0.177937318519413,
1.47769581483889));
#56682=CARTESIAN_POINT('Ctrl Pts',(-0.392296830459881,-0.0886050390430537,
1.47320608352119));
#56683=CARTESIAN_POINT('Ctrl Pts',(-0.392969983056837,0.000317581071747716,
1.4687163522035));
#56684=CARTESIAN_POINT('Ctrl Pts',(-0.39292938619043,0.000303368867518512,
1.4503836477965));
#56685=CARTESIAN_POINT('Ctrl Pts',(-0.392302731063306,-0.0869835717115683,
1.45478964484105));
#56686=CARTESIAN_POINT('Ctrl Pts',(-0.363610231497499,-0.174644473735395,
1.4591956418856));
#56687=CARTESIAN_POINT('Ctrl Pts',(-0.310148212606042,-0.242906048890095,
1.46360163893014));
#56688=CARTESIAN_POINT('Ctrl Pts',(-0.229807891961015,-0.345486477938193,
1.47022277338521));
#56689=CARTESIAN_POINT('Ctrl Pts',(-0.0935312385640766,-0.404257934004288,
1.47684390784028));
#56690=CARTESIAN_POINT('Ctrl Pts',(0.0362140774032489,-0.392280257494778,
1.48346504229536));
#56691=CARTESIAN_POINT('Ctrl Pts',(0.165959393370574,-0.380302580985268,
1.49008617675043));
#56692=CARTESIAN_POINT('Ctrl Pts',(0.289173371908287,-0.297575771900155,
1.4967073112055));
#56693=CARTESIAN_POINT('Ctrl Pts',(0.349376123956583,-0.182020843846168,
1.50332844566057));
#56694=CARTESIAN_POINT('Ctrl Pts',(0.409578876004877,-0.0664659157921843,
1.50994958011564));
#56695=CARTESIAN_POINT('Ctrl Pts',(0.406770401563758,0.0819171312306699,
1.51657071457071));
#56696=CARTESIAN_POINT('Ctrl Pts',(0.342238074307365,0.195111162240944,
1.52319184902578));
#56697=CARTESIAN_POINT('Ctrl Pts',(0.277705747050971,0.30830519325122,1.52981298348085));
#56698=CARTESIAN_POINT('Ctrl Pts',(0.151449566979302,0.386310208248916,
1.53643411793592));
#56699=CARTESIAN_POINT('Ctrl Pts',(0.0213439316380748,0.393369653966392,
1.54305525239099));
#56700=CARTESIAN_POINT('Ctrl Pts',(-0.108761703703154,0.400429099683869,
1.54967638684607));
#56701=CARTESIAN_POINT('Ctrl Pts',(-0.24271679431394,0.336542976121126,
1.55629752130114));
#56702=CARTESIAN_POINT('Ctrl Pts',(-0.319117844548307,0.230995842160026,
1.56291865575621));
#56703=CARTESIAN_POINT('Ctrl Pts',(-0.367062220722499,0.164761261886383,
1.56707365310297));
#56704=CARTESIAN_POINT('Ctrl Pts',(-0.392341764890002,0.0821205388687718,
1.57122865044974));
#56705=CARTESIAN_POINT('Ctrl Pts',(-0.392821510739754,-0.000250701325252446,
1.5753836477965));
#56706=CARTESIAN_POINT('Origin',(0.,0.,0.93));
#56707=CARTESIAN_POINT('',(-0.393805363403874,-0.000235004724456311,1.7187163522035));
#56708=CARTESIAN_POINT('',(-0.393842938295855,-0.000187384875455676,1.7003836477965));
#56709=CARTESIAN_POINT('',(-0.3933,-4.81653586104654E-17,0.93));
#56710=CARTESIAN_POINT('Ctrl Pts',(-0.393805363403874,-0.000235004724456311,
1.7187163522035));
#56711=CARTESIAN_POINT('Ctrl Pts',(-0.393042182615986,0.118159669343525,
1.71270522919364));
#56712=CARTESIAN_POINT('Ctrl Pts',(-0.336019807553631,0.237234833307885,
1.70669410618379));
#56713=CARTESIAN_POINT('Ctrl Pts',(-0.242886995036645,0.310176314488843,
1.70068298317393));
#56714=CARTESIAN_POINT('Ctrl Pts',(-0.140303023149369,0.390519929726693,
1.69406184871886));
#56715=CARTESIAN_POINT('Ctrl Pts',(0.00609226823398873,0.414891431126435,
1.68744071426379));
#56716=CARTESIAN_POINT('Ctrl Pts',(0.129185480108729,0.372158787137547,
1.68081957980872));
#56717=CARTESIAN_POINT('Ctrl Pts',(0.252278691983468,0.329426143148659,
1.67419844535365));
#56718=CARTESIAN_POINT('Ctrl Pts',(0.35206982434959,0.219589353771141,1.66757731089858));
#56719=CARTESIAN_POINT('Ctrl Pts',(0.382819647158814,0.0929757105602073,
1.66095617644351));
#56720=CARTESIAN_POINT('Ctrl Pts',(0.413569469968039,-0.0336379326507284,
1.65433504198844));
#56721=CARTESIAN_POINT('Ctrl Pts',(0.375277983220365,-0.177028429695081,
1.64771390753337));
#56722=CARTESIAN_POINT('Ctrl Pts',(0.285495539318975,-0.271456435539926,
1.64109277307829));
#56723=CARTESIAN_POINT('Ctrl Pts',(0.195713095417587,-0.365884441384768,
1.63447163862322));
#56724=CARTESIAN_POINT('Ctrl Pts',(0.0544396943624859,-0.411349956030106,
1.62785050416815));
#56725=CARTESIAN_POINT('Ctrl Pts',(-0.0735654818810781,-0.387017721917561,
1.62122936971308));
#56726=CARTESIAN_POINT('Ctrl Pts',(-0.201570658124644,-0.362685487805017,
1.61460823525801));
#56727=CARTESIAN_POINT('Ctrl Pts',(-0.316307609556672,-0.268555504934587,
1.60798710080294));
#56728=CARTESIAN_POINT('Ctrl Pts',(-0.36518277307682,-0.147772957765475,
1.60136596634787));
#56729=CARTESIAN_POINT('Ctrl Pts',(-0.384005133741704,-0.101258276256465,
1.59881609496641));
#56730=CARTESIAN_POINT('Ctrl Pts',(-0.393059503400641,-0.0507907411033471,
1.59626622358496));
#56731=CARTESIAN_POINT('Ctrl Pts',(-0.392790597751209,-0.000230484700094208,
1.5937163522035));
#56732=CARTESIAN_POINT('Ctrl Pts',(-0.392821510739754,-0.000250701325252446,
1.5753836477965));
#56733=CARTESIAN_POINT('Ctrl Pts',(-0.393106256780218,-0.0491409304027429,
1.57784978490481));
#56734=CARTESIAN_POINT('Ctrl Pts',(-0.38465443035242,-0.0979362249897565,
1.58031592201311));
#56735=CARTESIAN_POINT('Ctrl Pts',(-0.367019625039806,-0.143149829246245,
1.58278205912142));
#56736=CARTESIAN_POINT('Ctrl Pts',(-0.319673345438989,-0.264540222331967,
1.58940319357649));
#56737=CARTESIAN_POINT('Ctrl Pts',(-0.206133776379406,-0.360112864143958,
1.59602432803156));
#56738=CARTESIAN_POINT('Ctrl Pts',(-0.0784461550906783,-0.386058762652492,
1.60264546248663));
#56739=CARTESIAN_POINT('Ctrl Pts',(0.0492414661980497,-0.412004661161027,
1.60926659694171));
#56740=CARTESIAN_POINT('Ctrl Pts',(0.191077139715923,-0.368323816366105,
1.61588773139678));
#56741=CARTESIAN_POINT('Ctrl Pts',(0.282044980480955,-0.275038222919274,
1.62250886585185));
#56742=CARTESIAN_POINT('Ctrl Pts',(0.373012821245988,-0.181752629472443,
1.62913000030692));
#56743=CARTESIAN_POINT('Ctrl Pts',(0.41311282925818,-0.038862287373702,
1.63575113476199));
#56744=CARTESIAN_POINT('Ctrl Pts',(0.3839636600404,0.0881319427418194,1.64237226921706));
#56745=CARTESIAN_POINT('Ctrl Pts',(0.354814490822621,0.215126172857341,
1.64899340367213));
#56746=CARTESIAN_POINT('Ctrl Pts',(0.256416144374869,0.326224290989643,
1.6556145381272));
#56747=CARTESIAN_POINT('Ctrl Pts',(0.133873221284828,0.370503154207164,
1.66223567258227));
#56748=CARTESIAN_POINT('Ctrl Pts',(0.0113302981947858,0.414782017424686,
1.66885680703735));
#56749=CARTESIAN_POINT('Ctrl Pts',(-0.135357201537546,0.392241625727427,
1.67547794149242));
#56750=CARTESIAN_POINT('Ctrl Pts',(-0.238949232579617,0.313208538429519,
1.68209907594749));
#56751=CARTESIAN_POINT('Ctrl Pts',(-0.334307308924747,0.240457351909347,
1.68819393323049));
#56752=CARTESIAN_POINT('Ctrl Pts',(-0.393148487536621,0.119837142250066,
1.6942887905135));
#56753=CARTESIAN_POINT('Ctrl Pts',(-0.393842938295855,-0.000187384875455676,
1.7003836477965));
#56754=CARTESIAN_POINT('Origin',(0.,0.,-0.177777344927309));
#56755=CARTESIAN_POINT('',(-0.322689101172091,-0.000192565846880319,1.75972265507269));
#56756=CARTESIAN_POINT('',(-0.322321068793906,0.000363350312672553,1.78437734492731));
#56757=CARTESIAN_POINT('',(-0.322275,-2.94787261092574E-14,-0.177777344927309));
#56758=CARTESIAN_POINT('',(0.141600127780395,-0.29010115152588,1.8));
#56759=CARTESIAN_POINT('Ctrl Pts',(-0.322689101172091,-0.000192565846880313,
1.75972265507269));
#56760=CARTESIAN_POINT('Ctrl Pts',(-0.322752562984035,-0.0100375995009947,
1.76033266651791));
#56761=CARTESIAN_POINT('Ctrl Pts',(-0.317877158043228,-0.126673691476083,
1.76756381241819));
#56762=CARTESIAN_POINT('Ctrl Pts',(-0.180463403516937,-0.331269943931176,
1.78098959406063));
#56763=CARTESIAN_POINT('Ctrl Pts',(0.051569323594053,-0.333511267780158,
1.79380536425785));
#56764=CARTESIAN_POINT('Ctrl Pts',(0.141603157807413,-0.290105179958813,
1.8));
#56765=CARTESIAN_POINT('',(-0.227909696623847,-0.227855976023948,1.8));
#56766=CARTESIAN_POINT('Origin',(0.,0.,1.8));
#56767=CARTESIAN_POINT('Ctrl Pts',(-0.322321068793906,0.000363350312672563,
1.78437734492731));
#56768=CARTESIAN_POINT('Ctrl Pts',(-0.321520973335343,-0.0836845372725092,
1.78958489661821));
#56769=CARTESIAN_POINT('Ctrl Pts',(-0.287553299275345,-0.168198311462947,
1.7947924483091));
#56770=CARTESIAN_POINT('Ctrl Pts',(-0.227909696623847,-0.227855976023948,
1.8));
#56771=CARTESIAN_POINT('Origin',(0.,0.,-0.177777344927309));
#56772=CARTESIAN_POINT('',(-0.321857589347244,-0.000188862081689614,1.63472265507269));
#56773=CARTESIAN_POINT('',(-0.322719890514358,-0.000153545539665345,1.65937734492731));
#56774=CARTESIAN_POINT('',(-0.322275,-2.94787261092574E-14,-0.177777344927309));
#56775=CARTESIAN_POINT('Ctrl Pts',(-0.321857589347244,-0.000188862081689604,
1.63472265507269));
#56776=CARTESIAN_POINT('Ctrl Pts',(-0.322077934041294,-0.0416185763770278,
1.63727252645415));
#56777=CARTESIAN_POINT('Ctrl Pts',(-0.295393402245107,-0.190353673042667,
1.64644353229068));
#56778=CARTESIAN_POINT('Ctrl Pts',(-0.0711526387601384,-0.374320380910067,
1.66223567258227));
#56779=CARTESIAN_POINT('Ctrl Pts',(0.276131002163078,-0.262555325743576,
1.68209907594749));
#56780=CARTESIAN_POINT('Ctrl Pts',(0.370260589436959,0.089932640960989,
1.7019624793127));
#56781=CARTESIAN_POINT('Ctrl Pts',(0.124950237161653,0.359937608898739,
1.72182588267791));
#56782=CARTESIAN_POINT('Ctrl Pts',(-0.223872369623273,0.301866542751815,
1.74107927459791));
#56783=CARTESIAN_POINT('Ctrl Pts',(-0.322063741171035,0.0968215292084443,
1.75371153206284));
#56784=CARTESIAN_POINT('Ctrl Pts',(-0.322689101172091,-0.000192565846880313,
1.75972265507269));
#56785=CARTESIAN_POINT('Ctrl Pts',(-0.322719890514358,-0.000153545539665285,
1.65937734492731));
#56786=CARTESIAN_POINT('Ctrl Pts',(-0.322769025984903,-0.00864581304597595,
1.65990362209938));
#56787=CARTESIAN_POINT('Ctrl Pts',(-0.318611706634757,-0.12393053953812,
1.66705103372651));
#56788=CARTESIAN_POINT('Ctrl Pts',(-0.18032609112216,-0.335634029399439,
1.68081957980872));
#56789=CARTESIAN_POINT('Ctrl Pts',(0.184494543087876,-0.333417375353118,
1.70068298317393));
#56790=CARTESIAN_POINT('Ctrl Pts',(0.380171112467216,-0.0254013260161302,
1.72054638653915));
#56791=CARTESIAN_POINT('Ctrl Pts',(0.227322355071844,0.305652478161549,
1.74040978990436));
#56792=CARTESIAN_POINT('Ctrl Pts',(-0.133942736176479,0.356974128119761,
1.76027319326957));
#56793=CARTESIAN_POINT('Ctrl Pts',(-0.309881561511554,0.152660167939229,
1.77492904494389));
#56794=CARTESIAN_POINT('Ctrl Pts',(-0.322538253608777,0.023178034123378,
1.78296376216314));
#56795=CARTESIAN_POINT('Ctrl Pts',(-0.322321068793906,0.000363350312672563,
1.78437734492731));
#56796=CARTESIAN_POINT('Origin',(0.,0.,-0.177777344927309));
#56797=CARTESIAN_POINT('',(-0.322004579938068,0.000260229951415816,1.50972265507269));
#56798=CARTESIAN_POINT('',(-0.321882919841481,-0.000205427840351907,1.53437734492731));
#56799=CARTESIAN_POINT('',(-0.322275,-2.94787261092574E-14,-0.177777344927309));
#56800=CARTESIAN_POINT('Ctrl Pts',(-0.322004579938068,0.000260229951415825,
1.50972265507269));
#56801=CARTESIAN_POINT('Ctrl Pts',(-0.3214529901766,-0.0726040909168692,
1.51421238639039));
#56802=CARTESIAN_POINT('Ctrl Pts',(-0.26084449369421,-0.253754214926255,
1.52532325216316));
#56803=CARTESIAN_POINT('Ctrl Pts',(0.039813974270868,-0.378939562359927,
1.54305525239099));
#56804=CARTESIAN_POINT('Ctrl Pts',(0.340111362004286,-0.171769312742865,
1.56291865575621));
#56805=CARTESIAN_POINT('Ctrl Pts',(0.328602308377735,0.192875507586258,
1.58278205912142));
#56806=CARTESIAN_POINT('Ctrl Pts',(0.0158382535647818,0.380695741658215,
1.60264546248663));
#56807=CARTESIAN_POINT('Ctrl Pts',(-0.269432596141516,0.240196330941153,
1.61995899447039));
#56808=CARTESIAN_POINT('Ctrl Pts',(-0.321505775046774,0.065960068875241,
1.63065139199908));
#56809=CARTESIAN_POINT('Ctrl Pts',(-0.321857589347244,-0.000188862081689604,
1.63472265507269));
#56810=CARTESIAN_POINT('Ctrl Pts',(-0.321882919841481,-0.000205427840351873,
1.53437734492731));
#56811=CARTESIAN_POINT('Ctrl Pts',(-0.322116244352512,-0.0402667005989179,
1.53684348203562));
#56812=CARTESIAN_POINT('Ctrl Pts',(-0.296596899030457,-0.187598639238989,
1.54593075359899));
#56813=CARTESIAN_POINT('Ctrl Pts',(-0.0758728659140442,-0.373394473511197,
1.56163915961744));
#56814=CARTESIAN_POINT('Ctrl Pts',(0.272792974535782,-0.26601656156395,
1.58150256298265));
#56815=CARTESIAN_POINT('Ctrl Pts',(0.37136833748108,0.0852419052542959,
1.60136596634787));
#56816=CARTESIAN_POINT('Ctrl Pts',(0.129481784457052,0.358347519450231,
1.62122936971308));
#56817=CARTESIAN_POINT('Ctrl Pts',(-0.221557160855253,0.304405940632871,
1.64056649590623));
#56818=CARTESIAN_POINT('Ctrl Pts',(-0.322150848769053,0.0981960717483616,
1.65328248764431));
#56819=CARTESIAN_POINT('Ctrl Pts',(-0.322719890514358,-0.000153545539665285,
1.65937734492731));
#56820=CARTESIAN_POINT('Origin',(0.,0.,-0.177777344927309));
#56821=CARTESIAN_POINT('',(-0.322793653955721,5.74872430323103E-5,1.38472265507269));
#56822=CARTESIAN_POINT('',(-0.321971314351693,0.000248584291295761,1.40937734492731));
#56823=CARTESIAN_POINT('',(-0.322275,-2.94787261092574E-14,-0.177777344927309));
#56824=CARTESIAN_POINT('Ctrl Pts',(-0.322793653955721,5.74872430323201E-5,
1.38472265507269));
#56825=CARTESIAN_POINT('Ctrl Pts',(-0.322538771229688,-0.103631695006911,
1.39115224632663));
#56826=CARTESIAN_POINT('Ctrl Pts',(-0.212032190958281,-0.314565804986716,
1.40420297203564));
#56827=CARTESIAN_POINT('Ctrl Pts',(0.147397431593805,-0.351360758602383,
1.42387483219971));
#56828=CARTESIAN_POINT('Ctrl Pts',(0.375196172292565,-0.0663944216454938,
1.44373823556493));
#56829=CARTESIAN_POINT('Ctrl Pts',(0.259023581957562,0.279440820560319,
1.46360163893014));
#56830=CARTESIAN_POINT('Ctrl Pts',(-0.0946159429431672,0.369091050746847,
1.48346504229536));
#56831=CARTESIAN_POINT('Ctrl Pts',(-0.301186735501589,0.176586187251814,
1.49883871434287));
#56832=CARTESIAN_POINT('Ctrl Pts',(-0.322266435284178,0.034850995213737,
1.50759125193532));
#56833=CARTESIAN_POINT('Ctrl Pts',(-0.322004579938068,0.000260229951415825,
1.50972265507269));
#56834=CARTESIAN_POINT('Ctrl Pts',(-0.321971314351693,0.000248584291295775,
1.40937734492731));
#56835=CARTESIAN_POINT('Ctrl Pts',(-0.321457825205757,-0.0712754400542971,
1.41378334197186));
#56836=CARTESIAN_POINT('Ctrl Pts',(-0.262615556824558,-0.251049471647208,
1.42481047347147));
#56837=CARTESIAN_POINT('Ctrl Pts',(0.0350261341603416,-0.379412145143482,
1.44245873942616));
#56838=CARTESIAN_POINT('Ctrl Pts',(0.3379154166412,-0.176049960567548,1.46232214279137));
#56839=CARTESIAN_POINT('Ctrl Pts',(0.331011518086569,0.18871088214253,1.48218554615659));
#56840=CARTESIAN_POINT('Ctrl Pts',(0.0206437802330401,0.380465773129421,
1.5020489495218));
#56841=CARTESIAN_POINT('Ctrl Pts',(-0.267766340380685,0.242916654852083,
1.51944621577871));
#56842=CARTESIAN_POINT('Ctrl Pts',(-0.321489810017616,0.0672906093667012,
1.53022234758055));
#56843=CARTESIAN_POINT('Ctrl Pts',(-0.321882919841481,-0.000205427840351873,
1.53437734492731));
#56844=CARTESIAN_POINT('Origin',(0.,0.,-0.177777344927309));
#56845=CARTESIAN_POINT('',(-0.322175349074432,-0.000293111852957028,1.25972265507269));
#56846=CARTESIAN_POINT('',(-0.322780900192053,8.19532063371861E-5,1.28437734492731));
#56847=CARTESIAN_POINT('',(-0.322275,-2.94787261092574E-14,-0.177777344927309));
#56848=CARTESIAN_POINT('Ctrl Pts',(-0.322175349074432,-0.00029311185295702,
1.25972265507269));
#56849=CARTESIAN_POINT('Ctrl Pts',(-0.322427011010276,-0.0286286594376897,
1.2614709718078));
#56850=CARTESIAN_POINT('Ctrl Pts',(-0.306017829170326,-0.163988402508686,
1.26984042299797));
#56851=CARTESIAN_POINT('Ctrl Pts',(-0.115767935090022,-0.363012632792868,
1.28483100864322));
#56852=CARTESIAN_POINT('Ctrl Pts',(0.242457723385417,-0.293929649253331,
1.30469441200844));
#56853=CARTESIAN_POINT('Ctrl Pts',(0.378403647555055,0.0446213611812189,
1.32455781537365));
#56854=CARTESIAN_POINT('Ctrl Pts',(0.167437701577738,0.342264521233232,
1.34442121873886));
#56855=CARTESIAN_POINT('Ctrl Pts',(-0.197031326459517,0.326127341134279,
1.36428462210407));
#56856=CARTESIAN_POINT('Ctrl Pts',(-0.321360841411568,0.113006387783977,
1.37771843421535));
#56857=CARTESIAN_POINT('Ctrl Pts',(-0.322801247137205,0.00314647954545929,
1.38453111187156));
#56858=CARTESIAN_POINT('Ctrl Pts',(-0.322793653955721,5.74872430323201E-5,
1.38472265507269));
#56859=CARTESIAN_POINT('Ctrl Pts',(-0.322780900192053,8.195320633718E-5,
1.28437734492731));
#56860=CARTESIAN_POINT('Ctrl Pts',(-0.322432484508304,-0.102267719082872,
1.2907232019081));
#56861=CARTESIAN_POINT('Ctrl Pts',(-0.214459339993708,-0.312039456873427,
1.30369019334395));
#56862=CARTESIAN_POINT('Ctrl Pts',(0.142949239214434,-0.353193894022897,
1.32327831923488));
#56863=CARTESIAN_POINT('Ctrl Pts',(0.374327966327785,-0.0711265460495382,
1.3431417226001));
#56864=CARTESIAN_POINT('Ctrl Pts',(0.262531315278285,0.276148005038436,
1.36300512596531));
#56865=CARTESIAN_POINT('Ctrl Pts',(-0.0899480831884954,0.370256334701204,
1.38286852933052));
#56866=CARTESIAN_POINT('Ctrl Pts',(-0.300071343759289,0.179340842955076,
1.39832593565119));
#56867=CARTESIAN_POINT('Ctrl Pts',(-0.322229473629959,0.0362076510989722,
1.40716220751679));
#56868=CARTESIAN_POINT('Ctrl Pts',(-0.321971314351693,0.000248584291295775,
1.40937734492731));
#56869=CARTESIAN_POINT('Origin',(0.,0.,-0.177777344927309));
#56870=CARTESIAN_POINT('',(-0.321773287865446,9.92735819440501E-5,1.13472265507269));
#56871=CARTESIAN_POINT('',(-0.322215607507932,-0.000295487294752678,1.15937734492731));
#56872=CARTESIAN_POINT('',(-0.322275,-2.94787261092574E-14,-0.177777344927309));
#56873=CARTESIAN_POINT('Ctrl Pts',(-0.321773287865446,9.92735819440732E-5,
1.13472265507269));
#56874=CARTESIAN_POINT('Ctrl Pts',(-0.321607968139714,-0.0598645274198684,
1.13841083174404));
#56875=CARTESIAN_POINT('Ctrl Pts',(-0.276728969333462,-0.227707144521845,
1.14872014287045));
#56876=CARTESIAN_POINT('Ctrl Pts',(-0.00616808820702852,-0.380975512392104,
1.16565058845194));
#56877=CARTESIAN_POINT('Ctrl Pts',(0.316918362807963,-0.211525737604811,
1.18551399181716));
#56878=CARTESIAN_POINT('Ctrl Pts',(0.349461256362576,0.151846029436811,
1.20537739518237));
#56879=CARTESIAN_POINT('Ctrl Pts',(0.0616260067296811,0.376008805282698,
1.22524079854758));
#56880=CARTESIAN_POINT('Ctrl Pts',(-0.252399453807821,0.266066007796539,
1.24335588517769));
#56881=CARTESIAN_POINT('Ctrl Pts',(-0.3214739299804,0.0786822566276443,
1.25484983735273));
#56882=CARTESIAN_POINT('Ctrl Pts',(-0.322175349074432,-0.00029311185295702,
1.25972265507269));
#56883=CARTESIAN_POINT('Ctrl Pts',(-0.322215607507932,-0.000295487294752667,
1.15937734492731));
#56884=CARTESIAN_POINT('Ctrl Pts',(-0.322459681754105,-0.0272653545364726,
1.16104192738927));
#56885=CARTESIAN_POINT('Ctrl Pts',(-0.307015485637393,-0.161236448440899,
1.16932764430629));
#56886=CARTESIAN_POINT('Ctrl Pts',(-0.120342294288793,-0.361521982852271,
1.18423449567839));
#56887=CARTESIAN_POINT('Ctrl Pts',(0.238727114922392,-0.296967635404715,
1.2040978990436));
#56888=CARTESIAN_POINT('Ctrl Pts',(0.378936926926189,0.0398398957118962,
1.22396130240882));
#56889=CARTESIAN_POINT('Ctrl Pts',(0.171745970394351,0.34012311526861,1.24382470577403));
#56890=CARTESIAN_POINT('Ctrl Pts',(-0.192897791255575,0.328589187273149,
1.26368810913924));
#56891=CARTESIAN_POINT('Ctrl Pts',(-0.320700046313691,0.115736537458778,
1.27720565552367));
#56892=CARTESIAN_POINT('Ctrl Pts',(-0.322796014145884,0.00452178841960592,
1.28410206745303));
#56893=CARTESIAN_POINT('Ctrl Pts',(-0.322780900192053,8.195320633718E-5,
1.28437734492731));
#56894=CARTESIAN_POINT('Origin',(0.,0.,-0.177777344927309));
#56895=CARTESIAN_POINT('',(-0.322540009820288,0.000248098752203224,1.00972265507269));
#56896=CARTESIAN_POINT('',(-0.321762158101853,7.78407769116696E-5,1.03437734492731));
#56897=CARTESIAN_POINT('',(-0.322275,-2.94787261092574E-14,-0.177777344927309));
#56898=CARTESIAN_POINT('Ctrl Pts',(-0.322540009820288,0.000248098752203227,
1.00972265507269));
#56899=CARTESIAN_POINT('Ctrl Pts',(-0.321766175304399,-0.0907025733493005,
1.01535069168028));
#56900=CARTESIAN_POINT('Ctrl Pts',(-0.234056960396757,-0.289958622799939,
1.02759986274293));
#56901=CARTESIAN_POINT('Ctrl Pts',(0.103955810747213,-0.366570014821552,
1.04647016826066));
#56902=CARTESIAN_POINT('Ctrl Pts',(0.364453037776757,-0.111150211919144,
1.06633357162588));
#56903=CARTESIAN_POINT('Ctrl Pts',(0.290827996898553,0.246169580928165,
1.08619697499109));
#56904=CARTESIAN_POINT('Ctrl Pts',(-0.0494215465152554,0.377806692760261,
1.1060603783563));
#56905=CARTESIAN_POINT('Ctrl Pts',(-0.289598786989554,0.202949158922468,
1.12223560505017));
#56906=CARTESIAN_POINT('Ctrl Pts',(-0.32190475547657,0.04778443418078,1.13178969728897));
#56907=CARTESIAN_POINT('Ctrl Pts',(-0.321773287865446,9.92735819440732E-5,
1.13472265507269));
#56908=CARTESIAN_POINT('Ctrl Pts',(-0.321762158101853,7.78407769116314E-5,
1.03437734492731));
#56909=CARTESIAN_POINT('Ctrl Pts',(-0.321635720483669,-0.058529653262946,
1.03798178732551));
#56910=CARTESIAN_POINT('Ctrl Pts',(-0.278253620036456,-0.224969762308773,
1.04820736417877));
#56911=CARTESIAN_POINT('Ctrl Pts',(-0.0109779830180157,-0.380867294169285,
1.06505407548711));
#56912=CARTESIAN_POINT('Ctrl Pts',(0.314222297781658,-0.215510462520356,
1.08491747885232));
#56913=CARTESIAN_POINT('Ctrl Pts',(0.351350712306201,0.147421466689362,
1.10478088221754));
#56914=CARTESIAN_POINT('Ctrl Pts',(0.066368773346284,0.375200743340994,
1.12464428558275));
#56915=CARTESIAN_POINT('Ctrl Pts',(-0.250477710614327,0.268741916094579,
1.14284310648601));
#56916=CARTESIAN_POINT('Ctrl Pts',(-0.321488838652084,0.0800114679245235,
1.15442079293419));
#56917=CARTESIAN_POINT('Ctrl Pts',(-0.322215607507932,-0.000295487294752667,
1.15937734492731));
#56918=CARTESIAN_POINT('Origin',(0.,0.,-0.177777344927309));
#56919=CARTESIAN_POINT('',(-0.322560633728396,-0.000240562580560466,0.884722655072691));
#56920=CARTESIAN_POINT('',(-0.322501710998753,0.000260384004555324,0.90937734492731));
#56921=CARTESIAN_POINT('',(-0.322275,-2.94787261092574E-14,-0.177777344927309));
#56922=CARTESIAN_POINT('Ctrl Pts',(-0.322560633728396,-0.000240562580560428,
0.884722655072691));
#56923=CARTESIAN_POINT('Ctrl Pts',(-0.322688082286428,-0.0155379612308262,
0.885669417161446));
#56924=CARTESIAN_POINT('Ctrl Pts',(-0.31474304255412,-0.137683963102499,
0.893237313705273));
#56925=CARTESIAN_POINT('Ctrl Pts',(-0.158694433735999,-0.346405056336641,
0.90742634470417));
#56926=CARTESIAN_POINT('Ctrl Pts',(0.205247433654992,-0.321020057523545,
0.927289748069383));
#56927=CARTESIAN_POINT('Ctrl Pts',(0.381023115264154,-0.00133116068848917,
0.947153151434597));
#56928=CARTESIAN_POINT('Ctrl Pts',(0.207485458249651,0.319578114033663,
0.96701655479981));
#56929=CARTESIAN_POINT('Ctrl Pts',(-0.156270154667085,0.347505431777269,
0.986879958165023));
#56930=CARTESIAN_POINT('Ctrl Pts',(-0.314287675546238,0.139201754952349,
1.00111532492265));
#56931=CARTESIAN_POINT('Ctrl Pts',(-0.322676557153865,0.016296842388581,
1.00872955722521));
#56932=CARTESIAN_POINT('Ctrl Pts',(-0.322540009820288,0.000248098752203227,
1.00972265507269));
#56933=CARTESIAN_POINT('Ctrl Pts',(-0.322501710998753,0.000260384004555341,
0.90937734492731));
#56934=CARTESIAN_POINT('Ctrl Pts',(-0.321714914091844,-0.0893647805277536,
0.914921647261746));
#56935=CARTESIAN_POINT('Ctrl Pts',(-0.236204012765627,-0.287339077416759,
0.927087084051252));
#56936=CARTESIAN_POINT('Ctrl Pts',(0.0993190377930615,-0.367853422725428,
0.945873655295831));
#56937=CARTESIAN_POINT('Ctrl Pts',(0.363020578812783,-0.115743126091287,
0.965737058661042));
#56938=CARTESIAN_POINT('Ctrl Pts',(0.293913097770214,0.242477839890713,
0.985600462026258));
#56939=CARTESIAN_POINT('Ctrl Pts',(-0.0446472362210804,0.378400629197116,
1.00546386539147));
#56940=CARTESIAN_POINT('Ctrl Pts',(-0.288267845035054,0.20570020243003,
1.02172282635849));
#56941=CARTESIAN_POINT('Ctrl Pts',(-0.3218679784525,0.0491286348281514,
1.03136065287044));
#56942=CARTESIAN_POINT('Ctrl Pts',(-0.321762158101853,7.78407769116314E-5,
1.03437734492731));
#56943=CARTESIAN_POINT('Origin',(0.,0.,-0.177777344927309));
#56944=CARTESIAN_POINT('',(-0.321780623313585,-0.000110903176248464,0.759722655072691));
#56945=CARTESIAN_POINT('',(-0.322596689206338,-0.000225652695543505,0.78437734492731));
#56946=CARTESIAN_POINT('',(-0.322275,-2.94787261092574E-14,-0.177777344927309));
#56947=CARTESIAN_POINT('Ctrl Pts',(-0.321780623313585,-0.000110903176248449,
0.759722655072691));
#56948=CARTESIAN_POINT('Ctrl Pts',(-0.321925358645465,-0.0470400479730705,
0.762609277097686));
#56949=CARTESIAN_POINT('Ctrl Pts',(-0.290325268145637,-0.201426411122161,
0.772117033577752));
#56950=CARTESIAN_POINT('Ctrl Pts',(-0.0520601551526582,-0.377452151404502,
0.788245924512891));
#56951=CARTESIAN_POINT('Ctrl Pts',(0.289100858747305,-0.248195648281641,
0.808109327878104));
#56952=CARTESIAN_POINT('Ctrl Pts',(0.365220771143536,0.108600988391901,
0.827972731243317));
#56953=CARTESIAN_POINT('Ctrl Pts',(0.106514575117418,0.365834705354672,
0.84783613460853));
#56954=CARTESIAN_POINT('Ctrl Pts',(-0.23285652437024,0.291404635742235,
0.866752775884988));
#56955=CARTESIAN_POINT('Ctrl Pts',(-0.321796777016753,0.091443649544684,
0.879048282706375));
#56956=CARTESIAN_POINT('Ctrl Pts',(-0.322560633728396,-0.000240562580560428,
0.884722655072691));
#56957=CARTESIAN_POINT('Ctrl Pts',(-0.322596689206338,-0.00022565269554343,
0.78437734492731));
#56958=CARTESIAN_POINT('Ctrl Pts',(-0.322707672759724,-0.0141660460246545,
0.785240372742915));
#56959=CARTESIAN_POINT('Ctrl Pts',(-0.315551175979117,-0.134942160877861,
0.792724535013591));
#56960=CARTESIAN_POINT('Ctrl Pts',(-0.16305567921248,-0.344373717573672,
0.806829831739337));
#56961=CARTESIAN_POINT('Ctrl Pts',(0.201177731278749,-0.323586050868213,
0.826693235104551));
#56962=CARTESIAN_POINT('Ctrl Pts',(0.38097596669931,-0.00614204171891747,
0.846556638469764));
#56963=CARTESIAN_POINT('Ctrl Pts',(0.211504088229659,0.31693285178582,0.866420041834977));
#56964=CARTESIAN_POINT('Ctrl Pts',(-0.151869934840427,0.34945090466404,
0.88628344520019));
#56965=CARTESIAN_POINT('Ctrl Pts',(-0.313449894905197,0.141945587024724,
0.900602546230968));
#56966=CARTESIAN_POINT('Ctrl Pts',(-0.322654525208851,0.0176676699287391,
0.908300512806675));
#56967=CARTESIAN_POINT('Ctrl Pts',(-0.322501710998753,0.000260384004555341,
0.90937734492731));
#56968=CARTESIAN_POINT('Origin',(0.,0.,-0.177777344927309));
#56969=CARTESIAN_POINT('',(-0.322153421245596,0.000291028333709336,0.634722655072691));
#56970=CARTESIAN_POINT('',(-0.321795967956633,-0.000131423964174926,0.65937734492731));
#56971=CARTESIAN_POINT('',(-0.322275,-2.94787261092574E-14,-0.177777344927309));
#56972=CARTESIAN_POINT('Ctrl Pts',(-0.322153421245596,0.00029102833370933,
0.634722655072691));
#56973=CARTESIAN_POINT('Ctrl Pts',(-0.321467371001535,-0.0779468938575932,
0.639549137033926));
#56974=CARTESIAN_POINT('Ctrl Pts',(-0.253451104891186,-0.264582767850479,
0.650996753450233));
#56975=CARTESIAN_POINT('Ctrl Pts',(0.0589972495454716,-0.376430220494633,
0.66906550432161));
#56976=CARTESIAN_POINT('Ctrl Pts',(0.348391745474835,-0.154284082261366,
0.688928907686824));
#56977=CARTESIAN_POINT('Ctrl Pts',(0.318388601508794,0.209306198626352,
0.708792311052038));
#56978=CARTESIAN_POINT('Ctrl Pts',(-0.00350598136781482,0.381009310187041,
0.72865571441725));
#56979=CARTESIAN_POINT('Ctrl Pts',(-0.275874568389445,0.229220864270045,
0.745632495757469));
#56980=CARTESIAN_POINT('Ctrl Pts',(-0.32159337472638,0.0606027867557822,
0.755988142642615));
#56981=CARTESIAN_POINT('Ctrl Pts',(-0.321780623313585,-0.000110903176248449,
0.759722655072691));
#56982=CARTESIAN_POINT('Ctrl Pts',(-0.321795967956633,-0.000131423964174919,
0.65937734492731));
#56983=CARTESIAN_POINT('Ctrl Pts',(-0.321962962736951,-0.04569384867112,
0.662180232679155));
#56984=CARTESIAN_POINT('Ctrl Pts',(-0.291620126682177,-0.198673976518742,
0.671604254886071));
#56985=CARTESIAN_POINT('Ctrl Pts',(-0.0568219078975044,-0.376764757722924,
0.687649411548057));
#56986=CARTESIAN_POINT('Ctrl Pts',(0.285943996315395,-0.251826215573555,
0.707512814913272));
#56987=CARTESIAN_POINT('Ctrl Pts',(0.366562938806212,0.103980881765236,
0.727376218278483));
#56988=CARTESIAN_POINT('Ctrl Pts',(0.111125304043702,0.3644606682211,0.747239621643698));
#56989=CARTESIAN_POINT('Ctrl Pts',(-0.230664824743872,0.294011123707778,
0.766239997193306));
#56990=CARTESIAN_POINT('Ctrl Pts',(-0.321856208860203,0.0927844101711982,
0.778619238287844));
#56991=CARTESIAN_POINT('Ctrl Pts',(-0.322596689206338,-0.00022565269554343,
0.78437734492731));
#56992=CARTESIAN_POINT('Origin',(0.,0.,-0.177777344927309));
#56993=CARTESIAN_POINT('',(-0.322798898358608,-4.37237262256661E-5,0.50972265507269));
#56994=CARTESIAN_POINT('',(-0.322114562349406,0.000285900354075996,0.53437734492731));
#56995=CARTESIAN_POINT('',(-0.322275,-2.94787261092574E-14,-0.177777344927309));
#56996=CARTESIAN_POINT('Ctrl Pts',(-0.322798898358608,-4.37237262256363E-5,
0.50972265507269));
#56997=CARTESIAN_POINT('Ctrl Pts',(-0.322803350467903,-0.00238536310240654,
0.509867862515095));
#56998=CARTESIAN_POINT('Ctrl Pts',(-0.321718906904807,-0.111496286111473,
0.516634204412571));
#56999=CARTESIAN_POINT('Ctrl Pts',(-0.199305237284349,-0.324742680645371,
0.530021680765118));
#57000=CARTESIAN_POINT('Ctrl Pts',(0.16504213987037,-0.34342608880465,0.549885084130331));
#57001=CARTESIAN_POINT('Ctrl Pts',(0.378082631534635,-0.0472642580443332,
0.569748487495545));
#57002=CARTESIAN_POINT('Ctrl Pts',(0.244505553247802,0.29222837091975,0.589611890860758));
#57003=CARTESIAN_POINT('Ctrl Pts',(-0.113228663253673,0.363812666327059,
0.609475294225971));
#57004=CARTESIAN_POINT('Ctrl Pts',(-0.305456882130036,0.165511552441047,
0.624512215629949));
#57005=CARTESIAN_POINT('Ctrl Pts',(-0.322408518393226,0.0293825868023487,
0.632928002578855));
#57006=CARTESIAN_POINT('Ctrl Pts',(-0.322153421245596,0.00029102833370933,
0.634722655072691));
#57007=CARTESIAN_POINT('Ctrl Pts',(-0.322114562349406,0.000285900354075976,
0.53437734492731));
#57008=CARTESIAN_POINT('Ctrl Pts',(-0.321458474717958,-0.0766182390530337,
0.539120092615395));
#57009=CARTESIAN_POINT('Ctrl Pts',(-0.255330386675666,-0.261898064899981,
0.550483974758551));
#57010=CARTESIAN_POINT('Ctrl Pts',(0.0542395567617082,-0.377145174129293,
0.568468991356778));
#57011=CARTESIAN_POINT('Ctrl Pts',(0.346415935802215,-0.158670763850418,
0.588332394721992));
#57012=CARTESIAN_POINT('Ctrl Pts',(0.321006052375606,0.205269399120439,
0.608195798087205));
#57013=CARTESIAN_POINT('Ctrl Pts',(0.00130511053243591,0.381023238880027,
0.628059201452419));
#57014=CARTESIAN_POINT('Ctrl Pts',(-0.274311088907133,0.231954299418459,
0.645119717065786));
#57015=CARTESIAN_POINT('Ctrl Pts',(-0.321568478550757,0.0619361981922225,
0.655559098224084));
#57016=CARTESIAN_POINT('Ctrl Pts',(-0.321795967956633,-0.000131423964174919,
0.65937734492731));
#57017=CARTESIAN_POINT('Origin',(0.,0.,-0.177777344927309));
#57018=CARTESIAN_POINT('',(-0.322023724697603,-0.000266026364348698,0.38472265507269));
#57019=CARTESIAN_POINT('',(-0.322804887212102,-1.85792893697689E-5,0.40937734492731));
#57020=CARTESIAN_POINT('',(-0.322275,-2.94787261092574E-14,-0.177777344927309));
#57021=CARTESIAN_POINT('Ctrl Pts',(-0.322023724697603,-0.000266026364348675,
0.38472265507269));
#57022=CARTESIAN_POINT('Ctrl Pts',(-0.322286668321143,-0.0340997285001819,
0.386807722451335));
#57023=CARTESIAN_POINT('Ctrl Pts',(-0.301794699618203,-0.175061960972823,
0.395513924285051));
#57024=CARTESIAN_POINT('Ctrl Pts',(-0.0971925503173641,-0.368420939365887,
0.410841260573839));
#57025=CARTESIAN_POINT('Ctrl Pts',(0.257064747009525,-0.281243851578092,
0.430704663939052));
#57026=CARTESIAN_POINT('Ctrl Pts',(0.375650925262469,0.063771226098318,
0.450568067304265));
#57027=CARTESIAN_POINT('Ctrl Pts',(0.149848865235289,0.350322284637716,
0.470431470669478));
#57028=CARTESIAN_POINT('Ctrl Pts',(-0.210676274915335,0.315958889321312,
0.490149666592287));
#57029=CARTESIAN_POINT('Ctrl Pts',(-0.322600344246189,0.104388152760221,
0.503246728060024));
#57030=CARTESIAN_POINT('Ctrl Pts',(-0.322798898358608,-4.37237262256363E-5,
0.50972265507269));
#57031=CARTESIAN_POINT('Ctrl Pts',(-0.322804887212102,-1.85792893697065E-5,
0.40937734492731));
#57032=CARTESIAN_POINT('Ctrl Pts',(-0.322805713924285,-0.00100985665230741,
0.409438818096564));
#57033=CARTESIAN_POINT('Ctrl Pts',(-0.322352341065637,-0.108768573520454,
0.416121425720889));
#57034=CARTESIAN_POINT('Ctrl Pts',(-0.203389728683596,-0.32220029379513,
0.429425167800285));
#57035=CARTESIAN_POINT('Ctrl Pts',(0.160692729162575,-0.345482646427773,
0.449288571165499));
#57036=CARTESIAN_POINT('Ctrl Pts',(0.377455743121206,-0.0520343531991218,
0.469151974530712));
#57037=CARTESIAN_POINT('Ctrl Pts',(0.248175903852022,0.28911785229258,0.489015377895925));
#57038=CARTESIAN_POINT('Ctrl Pts',(-0.108625967532427,0.365213377502066,
0.508878781261139));
#57039=CARTESIAN_POINT('Ctrl Pts',(-0.304427023238494,0.168264571631386,
0.523999436938266));
#57040=CARTESIAN_POINT('Ctrl Pts',(-0.322374408836283,0.0307441341225915,
0.532498958160324));
#57041=CARTESIAN_POINT('Ctrl Pts',(-0.322114562349406,0.000285900354075976,
0.53437734492731));
#57042=CARTESIAN_POINT('Origin',(0.,0.,-0.177777344927309));
#57043=CARTESIAN_POINT('',(-0.321844616677633,0.000179048658294113,0.25972265507269));
#57044=CARTESIAN_POINT('',(-0.322059540737401,-0.000275272378033348,0.28437734492731));
#57045=CARTESIAN_POINT('',(-0.322275,-2.94787261092574E-14,-0.177777344927309));
#57046=CARTESIAN_POINT('Ctrl Pts',(-0.321844616677632,0.000179048658294108,
0.25972265507269));
#57047=CARTESIAN_POINT('Ctrl Pts',(-0.321515703515998,-0.0652236343715904,
0.263747582387576));
#57048=CARTESIAN_POINT('Ctrl Pts',(-0.270343504415437,-0.238689225402078,
0.274393644157532));
#57049=CARTESIAN_POINT('Ctrl Pts',(0.0131778654856828,-0.380797113767846,
0.291660840382558));
#57050=CARTESIAN_POINT('Ctrl Pts',(0.327246625055882,-0.195166812976406,
0.311524243747772));
#57051=CARTESIAN_POINT('Ctrl Pts',(0.341303248017118,0.169388689874893,
0.331387647112985));
#57052=CARTESIAN_POINT('Ctrl Pts',(0.0424607330362066,0.378652123483815,
0.351251050478199));
#57053=CARTESIAN_POINT('Ctrl Pts',(-0.259853013734845,0.255248969864476,
0.369029386464767));
#57054=CARTESIAN_POINT('Ctrl Pts',(-0.321451690467002,0.0733392412177939,
0.380186587996264));
#57055=CARTESIAN_POINT('Ctrl Pts',(-0.322023724697603,-0.000266026364348675,
0.38472265507269));
#57056=CARTESIAN_POINT('Ctrl Pts',(-0.322059540737401,-0.000275272378033303,
0.28437734492731));
#57057=CARTESIAN_POINT('Ctrl Pts',(-0.322322769946388,-0.032741145052682,
0.286378678032804));
#57058=CARTESIAN_POINT('Ctrl Pts',(-0.302876780071171,-0.172307827867515,
0.295001145593369));
#57059=CARTESIAN_POINT('Ctrl Pts',(-0.101836659246275,-0.367164356955896,
0.310244747609006));
#57060=CARTESIAN_POINT('Ctrl Pts',(0.25349314350919,-0.284467306274055,
0.330108150974219));
#57061=CARTESIAN_POINT('Ctrl Pts',(0.37642622426789,0.0590230048629484,
0.349971554339432));
#57062=CARTESIAN_POINT('Ctrl Pts',(0.154260273483973,0.348402316268487,
0.369834957704646));
#57063=CARTESIAN_POINT('Ctrl Pts',(-0.208202751865538,0.318467252949934,
0.389636887900605));
#57064=CARTESIAN_POINT('Ctrl Pts',(-0.322716670645885,0.105758360798129,
0.402817683641493));
#57065=CARTESIAN_POINT('Ctrl Pts',(-0.322804887212102,-1.85792893697065E-5,
0.40937734492731));
#57066=CARTESIAN_POINT('Origin',(0.,0.,-0.177777344927309));
#57067=CARTESIAN_POINT('',(-0.322672883777213,0.000203620636067219,0.13472265507269));
#57068=CARTESIAN_POINT('',(-0.321822258325956,0.000162574958589262,0.15937734492731));
#57069=CARTESIAN_POINT('',(-0.322275,-2.94787261092574E-14,-0.177777344927309));
#57070=CARTESIAN_POINT('Ctrl Pts',(-0.322672883777213,0.000203620636067221,
0.13472265507269));
#57071=CARTESIAN_POINT('Ctrl Pts',(-0.322020804100839,-0.096075831989152,
0.140687442323816));
#57072=CARTESIAN_POINT('Ctrl Pts',(-0.225137620539939,-0.300440548189766,
0.153273364030012));
#57073=CARTESIAN_POINT('Ctrl Pts',(0.122432227018064,-0.360801876178455,
0.172480420191279));
#57074=CARTESIAN_POINT('Ctrl Pts',(0.369623172725438,-0.0925175344721341,
0.192343823556493));
#57075=CARTESIAN_POINT('Ctrl Pts',(0.277958791015197,0.260619530981986,
0.212207226921706));
#57076=CARTESIAN_POINT('Ctrl Pts',(-0.0685354463999416,0.374808401925503,
0.232070630286919));
#57077=CARTESIAN_POINT('Ctrl Pts',(-0.294717851037753,0.191877835557772,
0.247909106337247));
#57078=CARTESIAN_POINT('Ctrl Pts',(-0.322056776210446,0.0423658757449738,
0.257126447932504));
#57079=CARTESIAN_POINT('Ctrl Pts',(-0.321844616677632,0.000179048658294108,
0.25972265507269));
#57080=CARTESIAN_POINT('Ctrl Pts',(-0.321822258325956,0.00016257495858928,
0.15937734492731));
#57081=CARTESIAN_POINT('Ctrl Pts',(-0.321535021268785,-0.0638911017945661,
0.163318537969044));
#57082=CARTESIAN_POINT('Ctrl Pts',(-0.271971025268605,-0.235966482044706,
0.17388086546585));
#57083=CARTESIAN_POINT('Ctrl Pts',(0.0083695466030628,-0.380931001484488,
0.191064327417726));
#57084=CARTESIAN_POINT('Ctrl Pts',(0.324755842971668,-0.199284387122036,
0.210927730782939));
#57085=CARTESIAN_POINT('Ctrl Pts',(0.343415090875769,0.165066330125723,
0.230791134148153));
#57086=CARTESIAN_POINT('Ctrl Pts',(0.0472382790882686,0.378085532147811,
0.250654537513366));
#57087=CARTESIAN_POINT('Ctrl Pts',(-0.258040470809522,0.25794659916087,
0.268516607773085));
#57088=CARTESIAN_POINT('Ctrl Pts',(-0.321451912426257,0.074667715366378,
0.279757543577733));
#57089=CARTESIAN_POINT('Ctrl Pts',(-0.322059540737401,-0.000275272378033303,
0.28437734492731));
#57090=CARTESIAN_POINT('Ctrl Pts',(-0.143290239521317,0.28866777250487,
0.0122936971308069));
#57091=CARTESIAN_POINT('Ctrl Pts',(-0.239363065031841,0.240978700533178,
0.018914831585878));
#57092=CARTESIAN_POINT('Ctrl Pts',(-0.378476748230256,0.0429489016361644,
0.0321571004960201));
#57093=CARTESIAN_POINT('Ctrl Pts',(-0.240846428651748,-0.295574326569485,
0.0520205038612334));
#57094=CARTESIAN_POINT('Ctrl Pts',(0.117909826126082,-0.362210109500856,
0.0718839072264466));
#57095=CARTESIAN_POINT('Ctrl Pts',(0.368403165707845,-0.0972337884399037,
0.09174731059166));
#57096=CARTESIAN_POINT('Ctrl Pts',(0.281239048491698,0.257118611189565,
0.111610713956873));
#57097=CARTESIAN_POINT('Ctrl Pts',(-0.0638035626910551,0.375628548193864,
0.131474117322087));
#57098=CARTESIAN_POINT('Ctrl Pts',(-0.350329092518743,0.1498343396268,0.1513375206873));
#57099=CARTESIAN_POINT('Ctrl Pts',(-0.315693082587524,-0.213357742304184,
0.171200924052513));
#57100=CARTESIAN_POINT('Ctrl Pts',(0.0083695466030628,-0.380931001484488,
0.191064327417726));
#57101=CARTESIAN_POINT('Ctrl Pts',(0.324755842971668,-0.199284387122036,
0.210927730782939));
#57102=CARTESIAN_POINT('Ctrl Pts',(0.343415090875769,0.165066330125723,
0.230791134148153));
#57103=CARTESIAN_POINT('Ctrl Pts',(0.0472382790882686,0.378085532147811,
0.250654537513366));
#57104=CARTESIAN_POINT('Ctrl Pts',(-0.292245042826693,0.244485784129382,
0.27051794087858));
#57105=CARTESIAN_POINT('Ctrl Pts',(-0.363804992481417,-0.113253645323718,
0.290381344243792));
#57106=CARTESIAN_POINT('Ctrl Pts',(-0.101836659246275,-0.367164356955896,
0.310244747609006));
#57107=CARTESIAN_POINT('Ctrl Pts',(0.25349314350919,-0.284467306274055,
0.330108150974219));
#57108=CARTESIAN_POINT('Ctrl Pts',(0.37642622426789,0.0590230048629484,
0.349971554339432));
#57109=CARTESIAN_POINT('Ctrl Pts',(0.154260273483973,0.348402316268487,
0.369834957704646));
#57110=CARTESIAN_POINT('Ctrl Pts',(-0.209327983127598,0.318374322452967,
0.389698361069859));
#57111=CARTESIAN_POINT('Ctrl Pts',(-0.381009103820433,-0.00353203298202855,
0.409561764435072));
#57112=CARTESIAN_POINT('Ctrl Pts',(-0.203389728683596,-0.32220029379513,
0.429425167800285));
#57113=CARTESIAN_POINT('Ctrl Pts',(0.160692729162575,-0.345482646427773,
0.449288571165499));
#57114=CARTESIAN_POINT('Ctrl Pts',(0.377455743121206,-0.0520343531991218,
0.469151974530712));
#57115=CARTESIAN_POINT('Ctrl Pts',(0.248175903852022,0.28911785229258,0.489015377895925));
#57116=CARTESIAN_POINT('Ctrl Pts',(-0.108625967532427,0.365213377502066,
0.508878781261139));
#57117=CARTESIAN_POINT('Ctrl Pts',(-0.365842018996859,0.106489572341696,
0.528742184626351));
#57118=CARTESIAN_POINT('Ctrl Pts',(-0.287662416064326,-0.249861454106355,
0.548605587991565));
#57119=CARTESIAN_POINT('Ctrl Pts',(0.0542395567617082,-0.377145174129293,
0.568468991356778));
#57120=CARTESIAN_POINT('Ctrl Pts',(0.346415935802215,-0.158670763850418,
0.588332394721992));
#57121=CARTESIAN_POINT('Ctrl Pts',(0.321006052375606,0.205269399120439,
0.608195798087205));
#57122=CARTESIAN_POINT('Ctrl Pts',(0.00130511053243591,0.381023238880027,
0.628059201452419));
#57123=CARTESIAN_POINT('Ctrl Pts',(-0.31959232700839,0.20746362668229,0.64792260481763));
#57124=CARTESIAN_POINT('Ctrl Pts',(-0.34749477743719,-0.156293926729706,
0.667786008182846));
#57125=CARTESIAN_POINT('Ctrl Pts',(-0.0568219078975044,-0.376764757722924,
0.687649411548057));
#57126=CARTESIAN_POINT('Ctrl Pts',(0.285943996315395,-0.251826215573555,
0.707512814913272));
#57127=CARTESIAN_POINT('Ctrl Pts',(0.366562938806212,0.103980881765236,
0.727376218278483));
#57128=CARTESIAN_POINT('Ctrl Pts',(0.111125304043702,0.3644606682211,0.747239621643698));
#57129=CARTESIAN_POINT('Ctrl Pts',(-0.246189485689262,0.290811191351024,
0.767103025008911));
#57130=CARTESIAN_POINT('Ctrl Pts',(-0.377803346174014,-0.0494473811102893,
0.786966428374124));
#57131=CARTESIAN_POINT('Ctrl Pts',(-0.16305567921248,-0.344373717573672,
0.806829831739337));
#57132=CARTESIAN_POINT('Ctrl Pts',(0.201177731278749,-0.323586050868213,
0.826693235104551));
#57133=CARTESIAN_POINT('Ctrl Pts',(0.38097596669931,-0.00614204171891747,
0.846556638469764));
#57134=CARTESIAN_POINT('Ctrl Pts',(0.211504088229659,0.31693285178582,0.866420041834977));
#57135=CARTESIAN_POINT('Ctrl Pts',(-0.151869934840427,0.34945090466404,
0.88628344520019));
#57136=CARTESIAN_POINT('Ctrl Pts',(-0.376013050780663,0.061600304557439,
0.906146848565404));
#57137=CARTESIAN_POINT('Ctrl Pts',(-0.255435941431669,-0.28272405575732,
0.926010251930617));
#57138=CARTESIAN_POINT('Ctrl Pts',(0.0993190377930615,-0.367853422725428,
0.945873655295831));
#57139=CARTESIAN_POINT('Ctrl Pts',(0.363020578812783,-0.115743126091287,
0.965737058661042));
#57140=CARTESIAN_POINT('Ctrl Pts',(0.293913097770214,0.242477839890713,
0.985600462026258));
#57141=CARTESIAN_POINT('Ctrl Pts',(-0.0446472362210804,0.378400629197116,
1.00546386539147));
#57142=CARTESIAN_POINT('Ctrl Pts',(-0.342275998032317,0.167414315546578,
1.02532726875668));
#57143=CARTESIAN_POINT('Ctrl Pts',(-0.326113898308744,-0.197053640435337,
1.0451906721219));
#57144=CARTESIAN_POINT('Ctrl Pts',(-0.0109779830180157,-0.380867294169285,
1.06505407548711));
#57145=CARTESIAN_POINT('Ctrl Pts',(0.314222297781658,-0.215510462520356,
1.08491747885232));
#57146=CARTESIAN_POINT('Ctrl Pts',(0.351350712306201,0.147421466689362,
1.10478088221754));
#57147=CARTESIAN_POINT('Ctrl Pts',(0.066368773346284,0.375200743340994,
1.12464428558275));
#57148=CARTESIAN_POINT('Ctrl Pts',(-0.279458549710258,0.259004499714875,
1.14450768894796));
#57149=CARTESIAN_POINT('Ctrl Pts',(-0.369084621200932,-0.0946411869735989,
1.16437109231318));
#57150=CARTESIAN_POINT('Ctrl Pts',(-0.120342294288793,-0.361521982852271,
1.18423449567839));
#57151=CARTESIAN_POINT('Ctrl Pts',(0.238727114922392,-0.296967635404715,
1.2040978990436));
#57152=CARTESIAN_POINT('Ctrl Pts',(0.378936926926189,0.0398398957118962,
1.22396130240882));
#57153=CARTESIAN_POINT('Ctrl Pts',(0.171745970394351,0.34012311526861,1.24382470577403));
#57154=CARTESIAN_POINT('Ctrl Pts',(-0.192897791255575,0.328589187273149,
1.26368810913924));
#57155=CARTESIAN_POINT('Ctrl Pts',(-0.380697238803822,0.0158121550827373,
1.28355151250445));
#57156=CARTESIAN_POINT('Ctrl Pts',(-0.219482103861983,-0.311461101926292,
1.30341491586967));
#57157=CARTESIAN_POINT('Ctrl Pts',(0.142949239214434,-0.353193894022897,
1.32327831923488));
#57158=CARTESIAN_POINT('Ctrl Pts',(0.374327966327785,-0.0711265460495382,
1.3431417226001));
#57159=CARTESIAN_POINT('Ctrl Pts',(0.262531315278285,0.276148005038436,
1.36300512596531));
#57160=CARTESIAN_POINT('Ctrl Pts',(-0.0899480831884954,0.370256334701204,
1.38286852933052));
#57161=CARTESIAN_POINT('Ctrl Pts',(-0.359965121917103,0.124922069524326,
1.40273193269573));
#57162=CARTESIAN_POINT('Ctrl Pts',(-0.299974311861765,-0.234937919333417,
1.42259533606095));
#57163=CARTESIAN_POINT('Ctrl Pts',(0.0350261341603416,-0.379412145143482,
1.44245873942616));
#57164=CARTESIAN_POINT('Ctrl Pts',(0.3379154166412,-0.176049960567548,1.46232214279137));
#57165=CARTESIAN_POINT('Ctrl Pts',(0.331011518086569,0.18871088214253,1.48218554615659));
#57166=CARTESIAN_POINT('Ctrl Pts',(0.0206437802330401,0.380465773129421,
1.5020489495218));
#57167=CARTESIAN_POINT('Ctrl Pts',(-0.308649711960631,0.223418477391944,
1.52191235288702));
#57168=CARTESIAN_POINT('Ctrl Pts',(-0.354980147521045,-0.138454174960786,
1.54177575625223));
#57169=CARTESIAN_POINT('Ctrl Pts',(-0.0758728659140442,-0.373394473511197,
1.56163915961744));
#57170=CARTESIAN_POINT('Ctrl Pts',(0.272792974535782,-0.26601656156395,
1.58150256298265));
#57171=CARTESIAN_POINT('Ctrl Pts',(0.37136833748108,0.0852419052542959,
1.60136596634787));
#57172=CARTESIAN_POINT('Ctrl Pts',(0.129481784457052,0.358347519450231,
1.62122936971308));
#57173=CARTESIAN_POINT('Ctrl Pts',(-0.231110999495935,0.302937872354617,
1.6410927730783));
#57174=CARTESIAN_POINT('Ctrl Pts',(-0.379825947107903,-0.0302167552855949,
1.66095617644351));
#57175=CARTESIAN_POINT('Ctrl Pts',(-0.18032609112216,-0.335634029399439,
1.68081957980872));
#57176=CARTESIAN_POINT('Ctrl Pts',(0.184494543087876,-0.333417375353118,
1.70068298317393));
#57177=CARTESIAN_POINT('Ctrl Pts',(0.380171112467216,-0.0254013260161302,
1.72054638653915));
#57178=CARTESIAN_POINT('Ctrl Pts',(0.227322355071844,0.305652478161549,
1.74040978990436));
#57179=CARTESIAN_POINT('Ctrl Pts',(-0.133942736176479,0.356974128119761,
1.76027319326957));
#57180=CARTESIAN_POINT('Ctrl Pts',(-0.372396558778726,0.0800628510138407,
1.78013659663479));
#57181=CARTESIAN_POINT('Ctrl Pts',(-0.303743473412038,-0.152004320240206,
1.79337886554493));
#57182=CARTESIAN_POINT('Ctrl Pts',(-0.227909696623847,-0.227855976023948,
1.8));
#57183=CARTESIAN_POINT('Ctrl Pts',(-0.153816642191914,0.309873914818277,
0.0259624647538713));
#57184=CARTESIAN_POINT('Ctrl Pts',(-0.256947179730866,0.258681503217605,
0.0325835992089423));
#57185=CARTESIAN_POINT('Ctrl Pts',(-0.40628044697931,0.0461040183726067,
0.0458258681190845));
#57186=CARTESIAN_POINT('Ctrl Pts',(-0.258539514365286,-0.317287838885153,
0.0656892714842978));
#57187=CARTESIAN_POINT('Ctrl Pts',(0.126571730194143,-0.388818826721966,
0.0855526748495111));
#57188=CARTESIAN_POINT('Ctrl Pts',(0.395466837876437,-0.104376787249354,
0.105416078214724));
#57189=CARTESIAN_POINT('Ctrl Pts',(0.301899461099073,0.276007085690883,
0.125279481579938));
#57190=CARTESIAN_POINT('Ctrl Pts',(-0.0684907067348376,0.403223012171802,
0.145142884945151));
#57191=CARTESIAN_POINT('Ctrl Pts',(-0.376065005218707,0.160841485668737,
0.165006288310364));
#57192=CARTESIAN_POINT('Ctrl Pts',(-0.338884561077199,-0.229031451245463,
0.184869691675577));
#57193=CARTESIAN_POINT('Ctrl Pts',(0.00898439111730312,-0.408914994844647,
0.20473309504079));
#57194=CARTESIAN_POINT('Ctrl Pts',(0.348613090919395,-0.213924237762373,
0.224596498406004));
#57195=CARTESIAN_POINT('Ctrl Pts',(0.368643086458686,0.177192450258299,
0.244459901771217));
#57196=CARTESIAN_POINT('Ctrl Pts',(0.0507085025229608,0.405860491339804,
0.264323305136431));
#57197=CARTESIAN_POINT('Ctrl Pts',(-0.313713978949325,0.262446224558406,
0.284186708501643));
#57198=CARTESIAN_POINT('Ctrl Pts',(-0.390530873164058,-0.121573496547171,
0.304050111866857));
#57199=CARTESIAN_POINT('Ctrl Pts',(-0.109317794635791,-0.394137023625451,
0.32391351523207));
#57200=CARTESIAN_POINT('Ctrl Pts',(0.272115283521848,-0.305364873494716,
0.343776918597283));
#57201=CARTESIAN_POINT('Ctrl Pts',(0.404079287209609,0.0633589590639552,
0.363640321962497));
#57202=CARTESIAN_POINT('Ctrl Pts',(0.165592557945175,0.373996683928579,
0.38350372532771));
#57203=CARTESIAN_POINT('Ctrl Pts',(-0.224705657475733,0.341762770468092,
0.403367128692924));
#57204=CARTESIAN_POINT('Ctrl Pts',(-0.408998834742623,-0.00379150356103331,
0.423230532058136));
#57205=CARTESIAN_POINT('Ctrl Pts',(-0.218331166358207,-0.345869805720036,
0.443093935423351));
#57206=CARTESIAN_POINT('Ctrl Pts',(0.17249755536046,-0.370862528994456,
0.462957338788562));
#57207=CARTESIAN_POINT('Ctrl Pts',(0.40518443668538,-0.0558569063353875,
0.482820742153777));
#57208=CARTESIAN_POINT('Ctrl Pts',(0.266407428244846,0.310357058414762,
0.502684145518989));
#57209=CARTESIAN_POINT('Ctrl Pts',(-0.116605859802474,0.392042721113458,
0.522547548884203));
#57210=CARTESIAN_POINT('Ctrl Pts',(-0.392717543935965,0.114312520523188,
0.542410952249416));
#57211=CARTESIAN_POINT('Ctrl Pts',(-0.308794702776989,-0.268216802569522,
0.562274355614629));
#57212=CARTESIAN_POINT('Ctrl Pts',(0.05822410879439,-0.404851052641468,
0.582137758979843));
#57213=CARTESIAN_POINT('Ctrl Pts',(0.371864379771239,-0.170327052219542,
0.602001162345056));
#57214=CARTESIAN_POINT('Ctrl Pts',(0.344587832811547,0.220348921342689,
0.621864565710269));
#57215=CARTESIAN_POINT('Ctrl Pts',(0.00140098669985904,0.409014008193454,
0.641727969075482));
#57216=CARTESIAN_POINT('Ctrl Pts',(-0.343070252202474,0.222704341480843,
0.661591372440696));
#57217=CARTESIAN_POINT('Ctrl Pts',(-0.373022475384054,-0.167775607639877,
0.681454775805909));
#57218=CARTESIAN_POINT('Ctrl Pts',(-0.060996164881367,-0.404442690044978,
0.701318179171122));
#57219=CARTESIAN_POINT('Ctrl Pts',(0.306950044295433,-0.270325899550608,
0.721181582536336));
#57220=CARTESIAN_POINT('Ctrl Pts',(0.393491424032298,0.111619536255318,
0.741044985901548));
#57221=CARTESIAN_POINT('Ctrl Pts',(0.119288802835838,0.391234716223999,
0.760908389266763));
#57222=CARTESIAN_POINT('Ctrl Pts',(-0.26427508362175,0.312174793725505,
0.780771792631975));
#57223=CARTESIAN_POINT('Ctrl Pts',(-0.405557575390273,-0.053079889830436,
0.800635195997189));
#57224=CARTESIAN_POINT('Ctrl Pts',(-0.17503409269586,-0.369672135892053,
0.820498599362402));
#57225=CARTESIAN_POINT('Ctrl Pts',(0.215956670966977,-0.347357363425207,
0.840362002727614));
#57226=CARTESIAN_POINT('Ctrl Pts',(0.408963263298817,-0.00659324903470751,
0.860225406092828));
#57227=CARTESIAN_POINT('Ctrl Pts',(0.227041623840047,0.340215406330941,
0.880088809458042));
#57228=CARTESIAN_POINT('Ctrl Pts',(-0.163026619992382,0.375122303835311,
0.899952212823254));
#57229=CARTESIAN_POINT('Ctrl Pts',(-0.403635761128137,0.0661255926201126,
0.919815616188469));
#57230=CARTESIAN_POINT('Ctrl Pts',(-0.274200803469975,-0.303493560124875,
0.93967901955368));
#57231=CARTESIAN_POINT('Ctrl Pts',(0.106615223410158,-0.394876709617135,
0.959542422918895));
#57232=CARTESIAN_POINT('Ctrl Pts',(0.389688834815862,-0.124245859813145,
0.979405826284108));
#57233=CARTESIAN_POINT('Ctrl Pts',(0.315504572720832,0.260290772508546,
0.999269229649321));
#57234=CARTESIAN_POINT('Ctrl Pts',(-0.0479271161917057,0.406198736081739,
1.01913263301453));
#57235=CARTESIAN_POINT('Ctrl Pts',(-0.367420313456767,0.179712923631493,
1.03899603637975));
#57236=CARTESIAN_POINT('Ctrl Pts',(-0.350070911860711,-0.211529615727575,
1.05885943974496));
#57237=CARTESIAN_POINT('Ctrl Pts',(-0.0117844487629612,-0.408846607455944,
1.07872284311017));
#57238=CARTESIAN_POINT('Ctrl Pts',(0.337305729322982,-0.231342314820938,
1.09858624647539));
#57239=CARTESIAN_POINT('Ctrl Pts',(0.377161675346616,0.15825135800538,1.1184496498406));
#57240=CARTESIAN_POINT('Ctrl Pts',(0.0712443631654572,0.402763779873762,
1.13831305320581));
#57241=CARTESIAN_POINT('Ctrl Pts',(-0.29998816312858,0.278031515557712,
1.15817645657103));
#57242=CARTESIAN_POINT('Ctrl Pts',(-0.396198354524746,-0.101593727821009,
1.17803985993624));
#57243=CARTESIAN_POINT('Ctrl Pts',(-0.129182892589275,-0.38808014884103,
1.19790326330145));
#57244=CARTESIAN_POINT('Ctrl Pts',(0.256264511387483,-0.318783503120817,
1.21776666666667));
#57245=CARTESIAN_POINT('Ctrl Pts',(0.406774431371081,0.0427666183276071,
1.23763007003188));
#57246=CARTESIAN_POINT('Ctrl Pts',(0.18436279096401,0.365109275392678,1.25749347339709));
#57247=CARTESIAN_POINT('Ctrl Pts',(-0.207068469117572,0.352728040763777,
1.27735687676231));
#57248=CARTESIAN_POINT('Ctrl Pts',(-0.408664059465309,0.0169737492851567,
1.29722028012752));
#57249=CARTESIAN_POINT('Ctrl Pts',(-0.235605721297195,-0.334341690206812,
1.31708368349273));
#57250=CARTESIAN_POINT('Ctrl Pts',(0.153450591284563,-0.379140261072753,
1.33694708685795));
#57251=CARTESIAN_POINT('Ctrl Pts',(0.401826886823667,-0.0763516518682445,
1.35681049022316));
#57252=CARTESIAN_POINT('Ctrl Pts',(0.281817418417573,0.296434418875328,
1.37667389358837));
#57253=CARTESIAN_POINT('Ctrl Pts',(-0.0965558587512498,0.39745614456561,
1.39653729695359));
#57254=CARTESIAN_POINT('Ctrl Pts',(-0.386408917623835,0.134099107755616,
1.4164007003188));
#57255=CARTESIAN_POINT('Ctrl Pts',(-0.322011056360493,-0.252196953512977,
1.43626410368402));
#57256=CARTESIAN_POINT('Ctrl Pts',(0.0375992277178473,-0.407284560119116,
1.45612750704922));
#57257=CARTESIAN_POINT('Ctrl Pts',(0.362739394576132,-0.188982961316714,
1.47599091041444));
#57258=CARTESIAN_POINT('Ctrl Pts',(0.355328321098593,0.202573980846195,
1.49585431377965));
#57259=CARTESIAN_POINT('Ctrl Pts',(0.0221603157912376,0.408415589835151,
1.51571771714486));
#57260=CARTESIAN_POINT('Ctrl Pts',(-0.331323769615328,0.239831269114091,
1.53558112051008));
#57261=CARTESIAN_POINT('Ctrl Pts',(-0.381057736513555,-0.148625310147182,
1.55544452387529));
#57262=CARTESIAN_POINT('Ctrl Pts',(-0.081446646382637,-0.400824817659447,
1.57530792724051));
#57263=CARTESIAN_POINT('Ctrl Pts',(0.292832920768453,-0.285558698233028,
1.59517133060572));
#57264=CARTESIAN_POINT('Ctrl Pts',(0.398649837410844,0.0915039550778764,
1.61503473397093));
#57265=CARTESIAN_POINT('Ctrl Pts',(0.138993788947073,0.384672482674136,
1.63489813733614));
#57266=CARTESIAN_POINT('Ctrl Pts',(-0.248088900087248,0.325192326246467,
1.65476154070136));
#57267=CARTESIAN_POINT('Ctrl Pts',(-0.407728760847038,-0.0324365417455611,
1.67462494406657));
#57268=CARTESIAN_POINT('Ctrl Pts',(-0.193573225424597,-0.360290411824483,
1.69448834743178));
#57269=CARTESIAN_POINT('Ctrl Pts',(0.198047900647739,-0.357910917705102,
1.714351750797));
#57270=CARTESIAN_POINT('Ctrl Pts',(0.408099282780338,-0.0272673609038275,
1.73421515416221));
#57271=CARTESIAN_POINT('Ctrl Pts',(0.244021933867365,0.328106352711155,
1.75407855752742));
#57272=CARTESIAN_POINT('Ctrl Pts',(-0.143782451571646,0.383198199125069,
1.77394196089264));
#57273=CARTESIAN_POINT('Ctrl Pts',(-0.399753594009775,0.0859444366092283,
1.79380536425785));
#57274=CARTESIAN_POINT('Ctrl Pts',(-0.326057108453634,-0.163170877626556,
1.80704763316799));
#57275=CARTESIAN_POINT('Ctrl Pts',(-0.244652422766334,-0.244594755738063,
1.81366876762306));
#57276=CARTESIAN_POINT('Ctrl Pts',(-0.164343044862511,0.331080057131683,
0.0396312323769356));
#57277=CARTESIAN_POINT('Ctrl Pts',(-0.274531294429891,0.276384305902031,
0.0462523668320067));
#57278=CARTESIAN_POINT('Ctrl Pts',(-0.434084145728363,0.0492591351090493,
0.0594946357421488));
#57279=CARTESIAN_POINT('Ctrl Pts',(-0.276232600078826,-0.339001351200821,
0.0793580391073622));
#57280=CARTESIAN_POINT('Ctrl Pts',(0.135233634262204,-0.415427543943075,
0.0992214424725753));
#57281=CARTESIAN_POINT('Ctrl Pts',(0.422530510045029,-0.111519786058804,
0.119084845837789));
#57282=CARTESIAN_POINT('Ctrl Pts',(0.322559873706447,0.294895560192201,
0.138948249203002));
#57283=CARTESIAN_POINT('Ctrl Pts',(-0.0731778507786196,0.430817476149739,
0.158811652568215));
#57284=CARTESIAN_POINT('Ctrl Pts',(-0.401800917918672,0.171848631710674,
0.178675055933429));
#57285=CARTESIAN_POINT('Ctrl Pts',(-0.362076039566874,-0.244705160186743,
0.198538459298642));
#57286=CARTESIAN_POINT('Ctrl Pts',(0.0095992356315428,-0.436898988204806,
0.218401862663855));
#57287=CARTESIAN_POINT('Ctrl Pts',(0.372470338867123,-0.228564088402712,
0.238265266029068));
#57288=CARTESIAN_POINT('Ctrl Pts',(0.393871082041601,0.189318570390874,
0.258128669394281));
#57289=CARTESIAN_POINT('Ctrl Pts',(0.0541787259576539,0.433635450531796,
0.277992072759495));
#57290=CARTESIAN_POINT('Ctrl Pts',(-0.335182915071958,0.28040666498743,
0.297855476124708));
#57291=CARTESIAN_POINT('Ctrl Pts',(-0.417256753846697,-0.129893347770624,
0.317718879489921));
#57292=CARTESIAN_POINT('Ctrl Pts',(-0.116798930025308,-0.421109690295005,
0.337582282855134));
#57293=CARTESIAN_POINT('Ctrl Pts',(0.290737423534506,-0.326262440715378,
0.357445686220348));
#57294=CARTESIAN_POINT('Ctrl Pts',(0.431732350151328,0.067694913264962,
0.377309089585562));
#57295=CARTESIAN_POINT('Ctrl Pts',(0.176924842406377,0.399591051588671,
0.397172492950774));
#57296=CARTESIAN_POINT('Ctrl Pts',(-0.240083331823868,0.365151218483217,
0.417035896315988));
#57297=CARTESIAN_POINT('Ctrl Pts',(-0.436988565664813,-0.00405097414003781,
0.4368992996812));
#57298=CARTESIAN_POINT('Ctrl Pts',(-0.233272604032816,-0.369539317644943,
0.456762703046414));
#57299=CARTESIAN_POINT('Ctrl Pts',(0.184302381558345,-0.396242411561139,
0.476626106411628));
#57300=CARTESIAN_POINT('Ctrl Pts',(0.432913130249555,-0.0596794594716531,
0.496489509776841));
#57301=CARTESIAN_POINT('Ctrl Pts',(0.284638952637669,0.331596264536944,
0.516352913142054));
#57302=CARTESIAN_POINT('Ctrl Pts',(-0.124585752072521,0.418872064724852,
0.536216316507267));
#57303=CARTESIAN_POINT('Ctrl Pts',(-0.419593068875071,0.12213546870468,
0.556079719872481));
#57304=CARTESIAN_POINT('Ctrl Pts',(-0.329926989489652,-0.28657215103269,
0.575943123237694));
#57305=CARTESIAN_POINT('Ctrl Pts',(0.0622086608270722,-0.432556931153643,
0.595806526602907));
#57306=CARTESIAN_POINT('Ctrl Pts',(0.397312823740262,-0.181983340588665,
0.615669929968121));
#57307=CARTESIAN_POINT('Ctrl Pts',(0.368169613247489,0.235428443564939,
0.635533333333333));
#57308=CARTESIAN_POINT('Ctrl Pts',(0.00149686286728203,0.437004777506881,
0.655396736698547));
#57309=CARTESIAN_POINT('Ctrl Pts',(-0.366548177396557,0.237945056279397,
0.675260140063759));
#57310=CARTESIAN_POINT('Ctrl Pts',(-0.398550173330919,-0.179257288550047,
0.695123543428974));
#57311=CARTESIAN_POINT('Ctrl Pts',(-0.0651704218652294,-0.432120622367032,
0.714986946794186));
#57312=CARTESIAN_POINT('Ctrl Pts',(0.327956092275469,-0.28882558352766,
0.7348503501594));
#57313=CARTESIAN_POINT('Ctrl Pts',(0.420419909258386,0.1192581907454,0.754713753524613));
#57314=CARTESIAN_POINT('Ctrl Pts',(0.127452301627973,0.418008764226898,
0.774577156889826));
#57315=CARTESIAN_POINT('Ctrl Pts',(-0.282360681554238,0.333538396099987,
0.79444056025504));
#57316=CARTESIAN_POINT('Ctrl Pts',(-0.433311804606533,-0.0567123985505825,
0.814303963620252));
#57317=CARTESIAN_POINT('Ctrl Pts',(-0.18701250617924,-0.394970554210435,
0.834167366985467));
#57318=CARTESIAN_POINT('Ctrl Pts',(0.230735610655205,-0.371128675982201,
0.854030770350678));
#57319=CARTESIAN_POINT('Ctrl Pts',(0.436950559898324,-0.00704445635049757,
0.873894173715893));
#57320=CARTESIAN_POINT('Ctrl Pts',(0.242579159450435,0.363497960876062,
0.893757577081105));
#57321=CARTESIAN_POINT('Ctrl Pts',(-0.174183305144337,0.400793703006583,
0.913620980446319));
#57322=CARTESIAN_POINT('Ctrl Pts',(-0.43125847147561,0.0706508806827865,
0.933484383811532));
#57323=CARTESIAN_POINT('Ctrl Pts',(-0.292965665508282,-0.324263064492431,
0.953347787176745));
#57324=CARTESIAN_POINT('Ctrl Pts',(0.113911409027256,-0.421899996508841,
0.97321119054196));
#57325=CARTESIAN_POINT('Ctrl Pts',(0.416357090818941,-0.132748593535004,
0.993074593907171));
#57326=CARTESIAN_POINT('Ctrl Pts',(0.33709604767145,0.278103705126378,1.01293799727239));
#57327=CARTESIAN_POINT('Ctrl Pts',(-0.0512069961623312,0.433996842966362,
1.0328014006376));
#57328=CARTESIAN_POINT('Ctrl Pts',(-0.392564628881217,0.192011531716408,
1.05266480400281));
#57329=CARTESIAN_POINT('Ctrl Pts',(-0.374027925412677,-0.226005591019812,
1.07252820736802));
#57330=CARTESIAN_POINT('Ctrl Pts',(-0.0125909145079066,-0.436825920742602,
1.09239161073324));
#57331=CARTESIAN_POINT('Ctrl Pts',(0.360389160864306,-0.24717416712152,
1.11225501409845));
#57332=CARTESIAN_POINT('Ctrl Pts',(0.402972638387031,0.169081249321399,
1.13211841746366));
#57333=CARTESIAN_POINT('Ctrl Pts',(0.0761199529846302,0.430326816406531,
1.15198182082888));
#57334=CARTESIAN_POINT('Ctrl Pts',(-0.320517776546902,0.297058531400549,
1.17184522419409));
#57335=CARTESIAN_POINT('Ctrl Pts',(-0.423312087848561,-0.10854626866842,
1.1917086275593));
#57336=CARTESIAN_POINT('Ctrl Pts',(-0.138023490889758,-0.414638314829788,
1.21157203092452));
#57337=CARTESIAN_POINT('Ctrl Pts',(0.273801907852573,-0.340599370836921,
1.23143543428973));
#57338=CARTESIAN_POINT('Ctrl Pts',(0.434611935815974,0.0456933409433185,
1.25129883765494));
#57339=CARTESIAN_POINT('Ctrl Pts',(0.196979611533669,0.390095435516746,
1.27116224102016));
#57340=CARTESIAN_POINT('Ctrl Pts',(-0.221239146979568,0.376866894254405,
1.29102564438537));
#57341=CARTESIAN_POINT('Ctrl Pts',(-0.436630880126795,0.018135343487576,
1.31088904775058));
#57342=CARTESIAN_POINT('Ctrl Pts',(-0.251729338732408,-0.357222278487332,
1.3307524511158));
#57343=CARTESIAN_POINT('Ctrl Pts',(0.163951943354692,-0.405086628122609,
1.35061585448101));
#57344=CARTESIAN_POINT('Ctrl Pts',(0.429325807319548,-0.0815767576869509,
1.37047925784622));
#57345=CARTESIAN_POINT('Ctrl Pts',(0.301103521556861,0.31672083271222,1.39034266121144));
#57346=CARTESIAN_POINT('Ctrl Pts',(-0.103163634314005,0.424655954430015,
1.41020606457665));
#57347=CARTESIAN_POINT('Ctrl Pts',(-0.412852713330567,0.143276145986907,
1.43006946794186));
#57348=CARTESIAN_POINT('Ctrl Pts',(-0.344047800859222,-0.269455987692538,
1.44993287130708));
#57349=CARTESIAN_POINT('Ctrl Pts',(0.0401723212753536,-0.435156975094748,
1.46979627467229));
#57350=CARTESIAN_POINT('Ctrl Pts',(0.387563372511063,-0.20191596206588,
1.4896596780375));
#57351=CARTESIAN_POINT('Ctrl Pts',(0.379645124110617,0.21643707954986,1.50952308140272));
#57352=CARTESIAN_POINT('Ctrl Pts',(0.0236768513494346,0.436365406540881,
1.52938648476793));
#57353=CARTESIAN_POINT('Ctrl Pts',(-0.353997827270024,0.256244060836238,
1.54924988813314));
#57354=CARTESIAN_POINT('Ctrl Pts',(-0.407135325506065,-0.158796445333579,
1.56911329149836));
#57355=CARTESIAN_POINT('Ctrl Pts',(-0.0870204268512302,-0.428255161807698,
1.58897669486357));
#57356=CARTESIAN_POINT('Ctrl Pts',(0.312872867001124,-0.305100834902106,
1.60884009822878));
#57357=CARTESIAN_POINT('Ctrl Pts',(0.425931337340609,0.0977660049014583,
1.628703501594));
#57358=CARTESIAN_POINT('Ctrl Pts',(0.148505793437094,0.410997445898041,
1.64856690495921));
#57359=CARTESIAN_POINT('Ctrl Pts',(-0.265066800678562,0.347446780138317,
1.66843030832442));
#57360=CARTESIAN_POINT('Ctrl Pts',(-0.435631574586173,-0.0346563282055276,
1.68829371168964));
#57361=CARTESIAN_POINT('Ctrl Pts',(-0.206820359727034,-0.384946794249528,
1.70815711505485));
#57362=CARTESIAN_POINT('Ctrl Pts',(0.211601258207602,-0.382404460057085,
1.72802051842006));
#57363=CARTESIAN_POINT('Ctrl Pts',(0.43602745309346,-0.0291333957915248,
1.74788392178528));
#57364=CARTESIAN_POINT('Ctrl Pts',(0.260721512662886,0.35056022726076,1.76774732515049));
#57365=CARTESIAN_POINT('Ctrl Pts',(-0.153622166966813,0.409422270130377,
1.7876107285157));
#57366=CARTESIAN_POINT('Ctrl Pts',(-0.427110629240823,0.0918260222046154,
1.80747413188091));
#57367=CARTESIAN_POINT('Ctrl Pts',(-0.34837074349523,-0.174337435012907,
1.82071640079106));
#57368=CARTESIAN_POINT('Ctrl Pts',(-0.261395148908821,-0.261333535452179,
1.82733753524613));
#57369=CARTESIAN_POINT('Ctrl Pts',(-0.174869447533108,0.35228619944509,
0.0533));
#57370=CARTESIAN_POINT('Ctrl Pts',(-0.292115409128916,0.294087108586458,
0.0599211344550711));
#57371=CARTESIAN_POINT('Ctrl Pts',(-0.461887844477417,0.0524142518454919,
0.0731634033652132));
#57372=CARTESIAN_POINT('Ctrl Pts',(-0.293925685792365,-0.36071486351649,
0.0930268067304267));
#57373=CARTESIAN_POINT('Ctrl Pts',(0.143895538330264,-0.442036261164184,
0.11289021009564));
#57374=CARTESIAN_POINT('Ctrl Pts',(0.449594182213621,-0.118662784868254,
0.132753613460853));
#57375=CARTESIAN_POINT('Ctrl Pts',(0.343220286313821,0.31378403469352,0.152617016826066));
#57376=CARTESIAN_POINT('Ctrl Pts',(-0.0778649948224021,0.458411940127677,
0.17248042019128));
#57377=CARTESIAN_POINT('Ctrl Pts',(-0.427536830618635,0.182855777752611,
0.192343823556493));
#57378=CARTESIAN_POINT('Ctrl Pts',(-0.385267518056549,-0.260378869128022,
0.212207226921706));
#57379=CARTESIAN_POINT('Ctrl Pts',(0.0102140801457829,-0.464882981564965,
0.232070630286919));
#57380=CARTESIAN_POINT('Ctrl Pts',(0.39632758681485,-0.243203939043049,
0.251934033652133));
#57381=CARTESIAN_POINT('Ctrl Pts',(0.419099077624518,0.201444690523449,
0.271797437017346));
#57382=CARTESIAN_POINT('Ctrl Pts',(0.0576489493923463,0.461410409723788,
0.291660840382559));
#57383=CARTESIAN_POINT('Ctrl Pts',(-0.35665185119459,0.298367105416454,
0.311524243747772));
#57384=CARTESIAN_POINT('Ctrl Pts',(-0.443982634529337,-0.138213198994076,
0.331387647112986));
#57385=CARTESIAN_POINT('Ctrl Pts',(-0.124280065414824,-0.44808235696456,
0.351251050478199));
#57386=CARTESIAN_POINT('Ctrl Pts',(0.309359563547165,-0.34716000793604,
0.371114453843412));
#57387=CARTESIAN_POINT('Ctrl Pts',(0.459385413093047,0.0720308674659688,
0.390977857208626));
#57388=CARTESIAN_POINT('Ctrl Pts',(0.188257126867579,0.425185419248763,
0.410841260573838));
#57389=CARTESIAN_POINT('Ctrl Pts',(-0.255461006172004,0.388539666498342,
0.430704663939053));
#57390=CARTESIAN_POINT('Ctrl Pts',(-0.464978296587002,-0.00431044471904228,
0.450568067304264));
#57391=CARTESIAN_POINT('Ctrl Pts',(-0.248214041707426,-0.39320882956985,
0.470431470669479));
#57392=CARTESIAN_POINT('Ctrl Pts',(0.19610720775623,-0.421622294127823,
0.490294874034691));
#57393=CARTESIAN_POINT('Ctrl Pts',(0.460641823813729,-0.0635020126079185,
0.510158277399905));
#57394=CARTESIAN_POINT('Ctrl Pts',(0.302870477030493,0.352835470659127,
0.530021680765118));
#57395=CARTESIAN_POINT('Ctrl Pts',(-0.132565644342568,0.445701408336244,
0.549885084130331));
#57396=CARTESIAN_POINT('Ctrl Pts',(-0.446468593814177,0.129958416886173,
0.569748487495545));
#57397=CARTESIAN_POINT('Ctrl Pts',(-0.351059276202315,-0.304927499495857,
0.589611890860758));
#57398=CARTESIAN_POINT('Ctrl Pts',(0.0661932128597544,-0.460262809665817,
0.609475294225972));
#57399=CARTESIAN_POINT('Ctrl Pts',(0.422761267709286,-0.193639628957789,
0.629338697591184));
#57400=CARTESIAN_POINT('Ctrl Pts',(0.39175139368343,0.250507965787189,0.649202100956398));
#57401=CARTESIAN_POINT('Ctrl Pts',(0.00159273903470509,0.464995546820308,
0.66906550432161));
#57402=CARTESIAN_POINT('Ctrl Pts',(-0.390026102590641,0.253185771077951,
0.688928907686825));
#57403=CARTESIAN_POINT('Ctrl Pts',(-0.424077871277783,-0.190738969460217,
0.708792311052037));
#57404=CARTESIAN_POINT('Ctrl Pts',(-0.0693446788490918,-0.459798554689087,
0.728655714417252));
#57405=CARTESIAN_POINT('Ctrl Pts',(0.348962140255506,-0.307325267504712,
0.748519117782463));
#57406=CARTESIAN_POINT('Ctrl Pts',(0.447348394484473,0.126896845235482,
0.768382521147677));
#57407=CARTESIAN_POINT('Ctrl Pts',(0.135615800420108,0.444782812229798,
0.788245924512891));
#57408=CARTESIAN_POINT('Ctrl Pts',(-0.300446279486727,0.354901998474468,
0.808109327878103));
#57409=CARTESIAN_POINT('Ctrl Pts',(-0.461066033822792,-0.0603449072707291,
0.827972731243318));
#57410=CARTESIAN_POINT('Ctrl Pts',(-0.198990919662619,-0.420268972528816,
0.84783613460853));
#57411=CARTESIAN_POINT('Ctrl Pts',(0.245514550343433,-0.394899988539195,
0.867699537973743));
#57412=CARTESIAN_POINT('Ctrl Pts',(0.464937856497831,-0.00749566366628734,
0.887562941338958));
#57413=CARTESIAN_POINT('Ctrl Pts',(0.258116695060824,0.386780515421183,
0.907426344704169));
#57414=CARTESIAN_POINT('Ctrl Pts',(-0.185339990296292,0.426465102177854,
0.927289748069384));
#57415=CARTESIAN_POINT('Ctrl Pts',(-0.458881181823084,0.0751761687454602,
0.947153151434596));
#57416=CARTESIAN_POINT('Ctrl Pts',(-0.311730527546589,-0.345032568859987,
0.96701655479981));
#57417=CARTESIAN_POINT('Ctrl Pts',(0.121207594644353,-0.448923283400548,
0.986879958165023));
#57418=CARTESIAN_POINT('Ctrl Pts',(0.44302534682202,-0.141251327256863,
1.00674336153024));
#57419=CARTESIAN_POINT('Ctrl Pts',(0.358687522622067,0.295916637744211,
1.02660676489545));
#57420=CARTESIAN_POINT('Ctrl Pts',(-0.0544868761329562,0.461794949850985,
1.04647016826066));
#57421=CARTESIAN_POINT('Ctrl Pts',(-0.417708944305668,0.204310139801323,
1.06633357162588));
#57422=CARTESIAN_POINT('Ctrl Pts',(-0.397984938964643,-0.24048156631205,
1.08619697499109));
#57423=CARTESIAN_POINT('Ctrl Pts',(-0.0133973802528527,-0.46480523402926,
1.1060603783563));
#57424=CARTESIAN_POINT('Ctrl Pts',(0.383472592405631,-0.263006019422102,
1.12592378172152));
#57425=CARTESIAN_POINT('Ctrl Pts',(0.428783601427445,0.179911140637417,
1.14578718508673));
#57426=CARTESIAN_POINT('Ctrl Pts',(0.080995542803804,0.457889852939299,
1.16565058845194));
#57427=CARTESIAN_POINT('Ctrl Pts',(-0.341047389965224,0.316085547243385,
1.18551399181716));
#57428=CARTESIAN_POINT('Ctrl Pts',(-0.450425821172375,-0.11549880951583,
1.20537739518237));
#57429=CARTESIAN_POINT('Ctrl Pts',(-0.14686408919024,-0.441196480818547,
1.22524079854758));
#57430=CARTESIAN_POINT('Ctrl Pts',(0.291339304317663,-0.362415238553024,
1.24510420191279));
#57431=CARTESIAN_POINT('Ctrl Pts',(0.462449440260866,0.0486200635590298,
1.26496760527801));
#57432=CARTESIAN_POINT('Ctrl Pts',(0.209596432103329,0.415081595640813,
1.28483100864322));
#57433=CARTESIAN_POINT('Ctrl Pts',(-0.235409824841565,0.401005747745034,
1.30469441200844));
#57434=CARTESIAN_POINT('Ctrl Pts',(-0.464597700788281,0.019296937689995,
1.32455781537365));
#57435=CARTESIAN_POINT('Ctrl Pts',(-0.26785295616762,-0.380102866767851,
1.34442121873886));
#57436=CARTESIAN_POINT('Ctrl Pts',(0.174453295424821,-0.431032995172465,
1.36428462210407));
#57437=CARTESIAN_POINT('Ctrl Pts',(0.45682472781543,-0.0868018635056573,
1.38414802546929));
#57438=CARTESIAN_POINT('Ctrl Pts',(0.320389624696148,0.337007246549112,
1.4040114288345));
#57439=CARTESIAN_POINT('Ctrl Pts',(-0.10977140987676,0.45185576429442,1.42387483219972));
#57440=CARTESIAN_POINT('Ctrl Pts',(-0.4392965090373,0.152453184218197,1.44373823556493));
#57441=CARTESIAN_POINT('Ctrl Pts',(-0.366084545357951,-0.286715021872099,
1.46360163893014));
#57442=CARTESIAN_POINT('Ctrl Pts',(0.0427454148328597,-0.463029390070381,
1.48346504229536));
#57443=CARTESIAN_POINT('Ctrl Pts',(0.412387350445995,-0.214848962815045,
1.50332844566057));
#57444=CARTESIAN_POINT('Ctrl Pts',(0.403961927122641,0.230300178253525,
1.52319184902578));
#57445=CARTESIAN_POINT('Ctrl Pts',(0.025193386907632,0.464315223246611,
1.54305525239099));
#57446=CARTESIAN_POINT('Ctrl Pts',(-0.376671884924722,0.272656852558385,
1.56291865575621));
#57447=CARTESIAN_POINT('Ctrl Pts',(-0.433212914498574,-0.168967580519975,
1.58278205912142));
#57448=CARTESIAN_POINT('Ctrl Pts',(-0.0925942073198233,-0.455685505955948,
1.60264546248664));
#57449=CARTESIAN_POINT('Ctrl Pts',(0.332912813233796,-0.324642971571184,
1.62250886585185));
#57450=CARTESIAN_POINT('Ctrl Pts',(0.453212837270372,0.104028054725039,
1.64237226921706));
#57451=CARTESIAN_POINT('Ctrl Pts',(0.158017797927116,0.437322409121946,
1.66223567258227));
#57452=CARTESIAN_POINT('Ctrl Pts',(-0.282044701269876,0.369701234030167,
1.68209907594749));
#57453=CARTESIAN_POINT('Ctrl Pts',(-0.463534388325307,-0.0368761146654934,
1.7019624793127));
#57454=CARTESIAN_POINT('Ctrl Pts',(-0.220067494029471,-0.409603176674573,
1.72182588267792));
#57455=CARTESIAN_POINT('Ctrl Pts',(0.225154615767464,-0.406898002409068,
1.74168928604313));
#57456=CARTESIAN_POINT('Ctrl Pts',(0.463955623406581,-0.0309994306792224,
1.76155268940834));
#57457=CARTESIAN_POINT('Ctrl Pts',(0.277421091458407,0.373014101810366,
1.78141609277355));
#57458=CARTESIAN_POINT('Ctrl Pts',(-0.16346188236198,0.435646341135685,
1.80127949613877));
#57459=CARTESIAN_POINT('Ctrl Pts',(-0.454467664471872,0.0977076078000029,
1.82114289950398));
#57460=CARTESIAN_POINT('Ctrl Pts',(-0.370684378536826,-0.185503992399258,
1.83438516841412));
#57461=CARTESIAN_POINT('Ctrl Pts',(-0.278137875051309,-0.278072315166294,
1.84100630286919));
#57462=CARTESIAN_POINT('',(-0.114300952321843,0.376324570415379,1.8));
#57463=CARTESIAN_POINT('Ctrl Pts',(-0.114617201976748,0.376923011799598,
1.8));
#57464=CARTESIAN_POINT('Ctrl Pts',(-0.122438613579645,0.373814783061767,
1.8));
#57465=CARTESIAN_POINT('Ctrl Pts',(-0.130137853077703,0.370443137950288,
1.8));
#57466=CARTESIAN_POINT('Ctrl Pts',(-0.137702035174531,0.366805935526825,
1.8));
#57467=CARTESIAN_POINT('Ctrl Pts',(-0.157131838454901,0.357463203335275,
1.8));
#57468=CARTESIAN_POINT('Ctrl Pts',(-0.175673019394112,0.346371270199071,
1.8));
#57469=CARTESIAN_POINT('Ctrl Pts',(-0.193189853500601,0.333742567265917,
1.8));
#57470=CARTESIAN_POINT('Ctrl Pts',(-0.203658595767835,0.326195162559511,
1.8));
#57471=CARTESIAN_POINT('Ctrl Pts',(-0.213760867036217,0.318097980230398,
1.8));
#57472=CARTESIAN_POINT('Ctrl Pts',(-0.223460905504529,0.309490823080894,
1.8));
#57473=CARTESIAN_POINT('Ctrl Pts',(-0.228445288511021,0.30506801919508,
1.8));
#57474=CARTESIAN_POINT('Ctrl Pts',(-0.233323372737349,0.30051050816285,
1.8));
#57475=CARTESIAN_POINT('Ctrl Pts',(-0.238089676004254,0.295823442462311,
1.8));
#57476=CARTESIAN_POINT('Ctrl Pts',(-0.242014920947028,0.291963452883965,
1.8));
#57477=CARTESIAN_POINT('Ctrl Pts',(-0.245858070184263,0.288021683976271,
1.8));
#57478=CARTESIAN_POINT('Ctrl Pts',(-0.249613876501175,0.284004910638523,
1.8));
#57479=CARTESIAN_POINT('Ctrl Pts',(-0.264084819509805,0.268528474117447,
1.8));
#57480=CARTESIAN_POINT('Ctrl Pts',(-0.277277817225154,0.251925602751329,
1.8));
#57481=CARTESIAN_POINT('Ctrl Pts',(-0.289049676537754,0.23438536611199,
1.8));
#57482=CARTESIAN_POINT('Ctrl Pts',(-0.29705015058476,0.222464546784734,
1.8));
#57483=CARTESIAN_POINT('Ctrl Pts',(-0.304393399646152,0.210110059716389,
1.8));
#57484=CARTESIAN_POINT('Ctrl Pts',(-0.311021403614141,0.197377127459023,
1.8));
#57485=CARTESIAN_POINT('Ctrl Pts',(-0.314228507045358,0.191216022105243,
1.8));
#57486=CARTESIAN_POINT('Ctrl Pts',(-0.317267976480838,0.184966286029691,
1.8));
#57487=CARTESIAN_POINT('Ctrl Pts',(-0.320132207960069,0.178634142888421,
1.8));
#57488=CARTESIAN_POINT('Ctrl Pts',(-0.322113958988996,0.174252956773918,
1.8));
#57489=CARTESIAN_POINT('Ctrl Pts',(-0.324010248252346,0.169835507334254,
1.8));
#57490=CARTESIAN_POINT('Ctrl Pts',(-0.325816003087781,0.1653916009695,1.8));
#57491=CARTESIAN_POINT('Ctrl Pts',(-0.333354523194409,0.146839537962231,
1.8));
#57492=CARTESIAN_POINT('Ctrl Pts',(-0.339336883851923,0.127787956818189,
1.8));
#57493=CARTESIAN_POINT('Ctrl Pts',(-0.343615830426459,0.108394982215767,
1.8));
#57494=CARTESIAN_POINT('Ctrl Pts',(-0.346015117263807,0.0975209720148686,
1.8));
#57495=CARTESIAN_POINT('Ctrl Pts',(-0.347877980992209,0.0865394609170954,
1.8));
#57496=CARTESIAN_POINT('Ctrl Pts',(-0.349171180768184,0.075478399293499,
1.8));
#57497=CARTESIAN_POINT('Ctrl Pts',(-0.350451949842727,0.0645236605730705,
1.8));
#57498=CARTESIAN_POINT('Ctrl Pts',(-0.351173826587271,0.0534908072357066,
1.8));
#57499=CARTESIAN_POINT('Ctrl Pts',(-0.351345950689055,0.0424165497826654,
1.8));
#57500=CARTESIAN_POINT('Ctrl Pts',(-0.351425035191472,0.0373283481233097,
1.8));
#57501=CARTESIAN_POINT('Ctrl Pts',(-0.351387829017759,0.0322398913435546,
1.8));
#57502=CARTESIAN_POINT('Ctrl Pts',(-0.351236346246636,0.0271582460828918,
1.8));
#57503=CARTESIAN_POINT('Ctrl Pts',(-0.350642909162813,0.00725078913467943,
1.8));
#57504=CARTESIAN_POINT('Ctrl Pts',(-0.348299967417274,-0.012571236927833,
1.8));
#57505=CARTESIAN_POINT('Ctrl Pts',(-0.344298540808079,-0.0320964970107567,
1.8));
#57506=CARTESIAN_POINT('Ctrl Pts',(-0.34158866400112,-0.0453195433430291,
1.8));
#57507=CARTESIAN_POINT('Ctrl Pts',(-0.338116987271259,-0.0584063854402795,
1.8));
#57508=CARTESIAN_POINT('Ctrl Pts',(-0.333899902424356,-0.07128511617414,
1.8));
#57509=CARTESIAN_POINT('Ctrl Pts',(-0.331891313091662,-0.0774192306417845,
1.8));
#57510=CARTESIAN_POINT('Ctrl Pts',(-0.329713494344077,-0.0835060326977867,
1.8));
#57511=CARTESIAN_POINT('Ctrl Pts',(-0.327367582606868,-0.0895371018240274,
1.8));
#57512=CARTESIAN_POINT('Ctrl Pts',(-0.325415778789272,-0.0945549648399598,
1.8));
#57513=CARTESIAN_POINT('Ctrl Pts',(-0.323351086569145,-0.0995252754617292,
1.8));
#57514=CARTESIAN_POINT('Ctrl Pts',(-0.321175405691638,-0.104442985850223,
1.8));
#57515=CARTESIAN_POINT('Ctrl Pts',(-0.315899089074665,-0.116369090137169,
1.8));
#57516=CARTESIAN_POINT('Ctrl Pts',(-0.309969963495991,-0.127987830133287,
1.8));
#57517=CARTESIAN_POINT('Ctrl Pts',(-0.303405158120671,-0.139233631733587,
1.8));
#57518=CARTESIAN_POINT('Ctrl Pts',(-0.299533235856367,-0.145866405609847,
1.8));
#57519=CARTESIAN_POINT('Ctrl Pts',(-0.295440032784457,-0.152369323019986,
1.8));
#57520=CARTESIAN_POINT('Ctrl Pts',(-0.291127918360532,-0.158727583407761,
1.8));
#57521=CARTESIAN_POINT('Ctrl Pts',(-0.287043388654486,-0.164750267613112,
1.8));
#57522=CARTESIAN_POINT('Ctrl Pts',(-0.282760740964221,-0.170644775881678,
1.8));
#57523=CARTESIAN_POINT('Ctrl Pts',(-0.278296041684024,-0.176380379709159,
1.8));
#57524=CARTESIAN_POINT('Ctrl Pts',(-0.266967254489208,-0.190933976965644,
1.8));
#57525=CARTESIAN_POINT('Ctrl Pts',(-0.254451318609441,-0.204494493516429,
1.8));
#57526=CARTESIAN_POINT('Ctrl Pts',(-0.240784361479587,-0.216852648005559,
1.8));
#57527=CARTESIAN_POINT('Ctrl Pts',(-0.236600651283484,-0.220635709330032,
1.8));
#57528=CARTESIAN_POINT('Ctrl Pts',(-0.232308897488585,-0.224305786482091,
1.8));
#57529=CARTESIAN_POINT('Ctrl Pts',(-0.227909696623847,-0.227855976023948,
1.8));
#57530=CARTESIAN_POINT('Ctrl Pts',(-0.393842938295855,-0.000187384875455676,
1.7003836477965));
#57531=CARTESIAN_POINT('Ctrl Pts',(-0.393902902551742,-0.0105512319322723,
1.70090992496857));
#57532=CARTESIAN_POINT('Ctrl Pts',(-0.393529328713883,-0.0209106376201641,
1.70143620214063));
#57533=CARTESIAN_POINT('Ctrl Pts',(-0.392708291433429,-0.0312344002177303,
1.7019624793127));
#57534=CARTESIAN_POINT('Ctrl Pts',(-0.382378756893362,-0.161118468668519,
1.70858361376777));
#57535=CARTESIAN_POINT('Ctrl Pts',(-0.301223125461419,-0.285360822671543,
1.71520474822284));
#57536=CARTESIAN_POINT('Ctrl Pts',(-0.186441624779293,-0.347031137295473,
1.72182588267791));
#57537=CARTESIAN_POINT('Ctrl Pts',(-0.0716601240971649,-0.408701451919404,
1.72844701713299));
#57538=CARTESIAN_POINT('Ctrl Pts',(0.0767472458351461,-0.407799727164238,
1.73506815158806));
#57539=CARTESIAN_POINT('Ctrl Pts',(0.190751098741156,-0.344699102831681,
1.74168928604313));
#57540=CARTESIAN_POINT('Ctrl Pts',(0.304754951647168,-0.281598478499124,
1.7483104204982));
#57541=CARTESIAN_POINT('Ctrl Pts',(0.384355287526875,-0.156298954589174,
1.75493155495327));
#57542=CARTESIAN_POINT('Ctrl Pts',(0.393066366808699,-0.0263136038859339,
1.76155268940834));
#57543=CARTESIAN_POINT('Ctrl Pts',(0.401777446090523,0.103671746817305,
1.76817382386341));
#57544=CARTESIAN_POINT('Ctrl Pts',(0.339599268774464,0.238342924313838,
1.77479495831848));
#57545=CARTESIAN_POINT('Ctrl Pts',(0.235029684479703,0.316117219616322,
1.78141609277355));
#57546=CARTESIAN_POINT('Ctrl Pts',(0.137195923693007,0.388881703221125,
1.7876107285157));
#57547=CARTESIAN_POINT('Ctrl Pts',(0.00225612663044948,0.411843221433994,
1.79380536425785));
#57548=CARTESIAN_POINT('Ctrl Pts',(-0.114617201976764,0.376923011799593,
1.8));
#57549=CARTESIAN_POINT('',(-0.187158653173899,-0.262360084935061,0.0533));
#57550=CARTESIAN_POINT('Ctrl Pts',(-0.187560716198532,-0.262742134024652,
0.0533));
#57551=CARTESIAN_POINT('Ctrl Pts',(-0.193636511193937,-0.259359136538732,
0.0533));
#57552=CARTESIAN_POINT('Ctrl Pts',(-0.19958510398352,-0.255771278629542,
0.0533));
#57553=CARTESIAN_POINT('Ctrl Pts',(-0.205394875738649,-0.251980685507045,
0.0533));
#57554=CARTESIAN_POINT('Ctrl Pts',(-0.217956745144151,-0.243784677508594,
0.0533));
#57555=CARTESIAN_POINT('Ctrl Pts',(-0.229870284953525,-0.234642384833593,
0.0533));
#57556=CARTESIAN_POINT('Ctrl Pts',(-0.241105135118966,-0.224672721347691,
0.0533));
#57557=CARTESIAN_POINT('Ctrl Pts',(-0.245472230993061,-0.220797415879949,
0.0533));
#57558=CARTESIAN_POINT('Ctrl Pts',(-0.249736686373294,-0.216796863541336,
0.0533000000000001));
#57559=CARTESIAN_POINT('Ctrl Pts',(-0.253896307158604,-0.212677223544441,
0.0533000000000001));
#57560=CARTESIAN_POINT('Ctrl Pts',(-0.258330366693657,-0.208285782604984,
0.0533000000000001));
#57561=CARTESIAN_POINT('Ctrl Pts',(-0.262639027648536,-0.203765130777088,
0.0533000000000001));
#57562=CARTESIAN_POINT('Ctrl Pts',(-0.266817483432449,-0.199126826877465,
0.0533000000000001));
#57563=CARTESIAN_POINT('Ctrl Pts',(-0.275301291296798,-0.18970935756922,
0.0533000000000001));
#57564=CARTESIAN_POINT('Ctrl Pts',(-0.283252555387633,-0.17980358772735,
0.0533));
#57565=CARTESIAN_POINT('Ctrl Pts',(-0.290652088370279,-0.169475045182507,
0.0533));
#57566=CARTESIAN_POINT('Ctrl Pts',(-0.295150312948837,-0.163196256501539,
0.0533));
#57567=CARTESIAN_POINT('Ctrl Pts',(-0.29944455411437,-0.156761050609704,
0.0533));
#57568=CARTESIAN_POINT('Ctrl Pts',(-0.303529464395936,-0.150182734495315,
0.0533));
#57569=CARTESIAN_POINT('Ctrl Pts',(-0.307092531148336,-0.144444792210579,
0.0533));
#57570=CARTESIAN_POINT('Ctrl Pts',(-0.310497232713595,-0.138595640257259,
0.0533));
#57571=CARTESIAN_POINT('Ctrl Pts',(-0.313728903073767,-0.132664844733238,
0.0533));
#57572=CARTESIAN_POINT('Ctrl Pts',(-0.323341236409495,-0.115024189230276,
0.0533));
#57573=CARTESIAN_POINT('Ctrl Pts',(-0.331449415040724,-0.0966280872271142,
0.0533));
#57574=CARTESIAN_POINT('Ctrl Pts',(-0.337977761615037,-0.0777141154187473,
0.0533));
#57575=CARTESIAN_POINT('Ctrl Pts',(-0.34214350835192,-0.0656450845477116,
0.0533));
#57576=CARTESIAN_POINT('Ctrl Pts',(-0.345665382203141,-0.0533642266892958,
0.0533000000000001));
#57577=CARTESIAN_POINT('Ctrl Pts',(-0.348515086834976,-0.0409264571618923,
0.0533000000000001));
#57578=CARTESIAN_POINT('Ctrl Pts',(-0.350083642823025,-0.0340803659381738,
0.0533000000000001));
#57579=CARTESIAN_POINT('Ctrl Pts',(-0.351448420077869,-0.0271866616054783,
0.0533));
#57580=CARTESIAN_POINT('Ctrl Pts',(-0.352603627980865,-0.0202541240282325,
0.0533));
#57581=CARTESIAN_POINT('Ctrl Pts',(-0.353341821950461,-0.0158241357808845,
0.0533));
#57582=CARTESIAN_POINT('Ctrl Pts',(-0.353994073919582,-0.011379600904418,
0.0533));
#57583=CARTESIAN_POINT('Ctrl Pts',(-0.354557987170772,-0.00693268604601465,
0.0533));
#57584=CARTESIAN_POINT('Ctrl Pts',(-0.356544004100534,0.00872867352545007,
0.0533));
#57585=CARTESIAN_POINT('Ctrl Pts',(-0.357441243642084,0.0244515531282482,
0.0533));
#57586=CARTESIAN_POINT('Ctrl Pts',(-0.357208358621734,0.0401306151146961,
0.0533));
#57587=CARTESIAN_POINT('Ctrl Pts',(-0.356976992543487,0.0557074138153622,
0.0533));
#57588=CARTESIAN_POINT('Ctrl Pts',(-0.355630556643009,0.0712413952181323,
0.0533));
#57589=CARTESIAN_POINT('Ctrl Pts',(-0.353239351858838,0.0866540484795216,
0.0533));
#57590=CARTESIAN_POINT('Ctrl Pts',(-0.352085419540309,0.0940917881621845,
0.0533));
#57591=CARTESIAN_POINT('Ctrl Pts',(-0.350687882387897,0.101501314598154,
0.0533));
#57592=CARTESIAN_POINT('Ctrl Pts',(-0.349053024053041,0.10887384878209,
0.0533));
#57593=CARTESIAN_POINT('Ctrl Pts',(-0.347355284894117,0.116529949447026,
0.0533));
#57594=CARTESIAN_POINT('Ctrl Pts',(-0.345399312227588,0.124152796342384,
0.0533));
#57595=CARTESIAN_POINT('Ctrl Pts',(-0.343202678426538,0.131696252532374,
0.0533));
#57596=CARTESIAN_POINT('Ctrl Pts',(-0.33743136038184,0.151515525461643,
0.0533));
#57597=CARTESIAN_POINT('Ctrl Pts',(-0.329997551557849,0.170823614573644,
0.0533));
#57598=CARTESIAN_POINT('Ctrl Pts',(-0.321061225945632,0.189447349149852,
0.0533));
#57599=CARTESIAN_POINT('Ctrl Pts',(-0.313086943720081,0.206066138801092,
0.0533));
#57600=CARTESIAN_POINT('Ctrl Pts',(-0.303915204286004,0.222140756471803,
0.0533));
#57601=CARTESIAN_POINT('Ctrl Pts',(-0.2936268562705,0.237543508329172,0.0533));
#57602=CARTESIAN_POINT('Ctrl Pts',(-0.290722215070209,0.241892065315711,
0.0533));
#57603=CARTESIAN_POINT('Ctrl Pts',(-0.287728400765138,0.246187004087764,
0.0533));
#57604=CARTESIAN_POINT('Ctrl Pts',(-0.284646842060306,0.250425257901783,
0.0533));
#57605=CARTESIAN_POINT('Ctrl Pts',(-0.281599100702271,0.254617000676173,
0.0533));
#57606=CARTESIAN_POINT('Ctrl Pts',(-0.278470738930216,0.258746075409449,
0.0533));
#57607=CARTESIAN_POINT('Ctrl Pts',(-0.275265448025107,0.262808141138579,
0.0533));
#57608=CARTESIAN_POINT('Ctrl Pts',(-0.261269669386206,0.280544993875083,
0.0533));
#57609=CARTESIAN_POINT('Ctrl Pts',(-0.245803353568857,0.297017252463422,
0.0533));
#57610=CARTESIAN_POINT('Ctrl Pts',(-0.229026180874183,0.312007620837193,
0.0533000000000001));
#57611=CARTESIAN_POINT('Ctrl Pts',(-0.213164506043965,0.326179993802361,
0.0533000000000001));
#57612=CARTESIAN_POINT('Ctrl Pts',(-0.196130043934341,0.339029002927305,
0.0533));
#57613=CARTESIAN_POINT('Ctrl Pts',(-0.178016632246539,0.350342635307754,
0.0533));
#57614=CARTESIAN_POINT('Ctrl Pts',(-0.176971169526133,0.350995631059742,
0.0533));
#57615=CARTESIAN_POINT('Ctrl Pts',(-0.175922103056024,0.351643500814262,
0.0533));
#57616=CARTESIAN_POINT('Ctrl Pts',(-0.174869447533108,0.35228619944509,
0.0533));
#57617=CARTESIAN_POINT('Ctrl Pts',(-0.18756071619853,-0.262742134024653,
0.0533000000000001));
#57618=CARTESIAN_POINT('Ctrl Pts',(-0.105929749524472,-0.320418481561441,
0.059494635742149));
#57619=CARTESIAN_POINT('Ctrl Pts',(0.123288314644033,-0.356520648444787,
0.0723104059393689));
#57620=CARTESIAN_POINT('Ctrl Pts',(0.368403165707845,-0.0972337884399037,
0.09174731059166));
#57621=CARTESIAN_POINT('Ctrl Pts',(0.281239048491698,0.257118611189565,
0.111610713956873));
#57622=CARTESIAN_POINT('Ctrl Pts',(-0.0638035626910551,0.375628548193864,
0.131474117322087));
#57623=CARTESIAN_POINT('Ctrl Pts',(-0.293478189192993,0.194635250493208,
0.147396327645565));
#57624=CARTESIAN_POINT('Ctrl Pts',(-0.322017574433746,0.0437179398416368,
0.156697403513973));
#57625=CARTESIAN_POINT('Ctrl Pts',(-0.321822258325956,0.00016257495858928,
0.15937734492731));
#57626=CARTESIAN_POINT('Origin',(-5.160062080289E-17,2.1385152528819E-17,
0.0533));
#57627=CARTESIAN_POINT('',(-0.3933,-4.81653586104654E-17,0.0533000000000001));
#57628=CARTESIAN_POINT('Origin',(0.,0.,0.0533));
#57629=CARTESIAN_POINT('Origin',(0.,0.,0.0533));
#57630=CARTESIAN_POINT('',(0.187158653173902,-0.262360084935058,0.0533));
#57631=CARTESIAN_POINT('Ctrl Pts',(0.175280092543415,0.352824285593914,
0.0533));
#57632=CARTESIAN_POINT('Ctrl Pts',(0.182476661777002,0.348469857043458,
0.0533));
#57633=CARTESIAN_POINT('Ctrl Pts',(0.189513753595691,0.343873471838117,
0.0532999999999999));
#57634=CARTESIAN_POINT('Ctrl Pts',(0.196377574736944,0.339034381908458,
0.0532999999999999));
#57635=CARTESIAN_POINT('Ctrl Pts',(0.209106724890824,0.330060152968759,
0.0532999999999999));
#57636=CARTESIAN_POINT('Ctrl Pts',(0.221240628245203,0.320251656613418,
0.0533));
#57637=CARTESIAN_POINT('Ctrl Pts',(0.232739197742172,0.309694329310758,
0.0533));
#57638=CARTESIAN_POINT('Ctrl Pts',(0.23985544575162,0.303160598360795,0.0533));
#57639=CARTESIAN_POINT('Ctrl Pts',(0.246728142345483,0.296339860335349,
0.0533));
#57640=CARTESIAN_POINT('Ctrl Pts',(0.25334550097625,0.289251071117036,0.0533));
#57641=CARTESIAN_POINT('Ctrl Pts',(0.257726631531975,0.284557822227207,
0.0533));
#57642=CARTESIAN_POINT('Ctrl Pts',(0.261988647138667,0.279754733652569,
0.0533000000000001));
#57643=CARTESIAN_POINT('Ctrl Pts',(0.266128947248262,0.274848072424167,
0.0533));
#57644=CARTESIAN_POINT('Ctrl Pts',(0.280033143836886,0.258370237362071,
0.0533));
#57645=CARTESIAN_POINT('Ctrl Pts',(0.292568657834103,0.24072534694436,0.0533));
#57646=CARTESIAN_POINT('Ctrl Pts',(0.303609786261102,0.222132165374485,
0.0533));
#57647=CARTESIAN_POINT('Ctrl Pts',(0.306585509497727,0.21712106865497,0.0533));
#57648=CARTESIAN_POINT('Ctrl Pts',(0.309453480170002,0.212038981971964,
0.0533));
#57649=CARTESIAN_POINT('Ctrl Pts',(0.312207122974928,0.206896593722832,
0.0533));
#57650=CARTESIAN_POINT('Ctrl Pts',(0.322145270739341,0.188337246014253,
0.0533));
#57651=CARTESIAN_POINT('Ctrl Pts',(0.33056064005666,0.169066507843323,0.0533000000000001));
#57652=CARTESIAN_POINT('Ctrl Pts',(0.337346359383174,0.149290670646457,
0.0533000000000001));
#57653=CARTESIAN_POINT('Ctrl Pts',(0.343948622498527,0.130049485708268,
0.0533000000000001));
#57654=CARTESIAN_POINT('Ctrl Pts',(0.349008411343874,0.11032878114862,0.0533));
#57655=CARTESIAN_POINT('Ctrl Pts',(0.352378978874987,0.0903158693762518,
0.0533));
#57656=CARTESIAN_POINT('Ctrl Pts',(0.353314918731474,0.0847586800901094,
0.0533));
#57657=CARTESIAN_POINT('Ctrl Pts',(0.354120303577725,0.0791790087202579,
0.0533));
#57658=CARTESIAN_POINT('Ctrl Pts',(0.354791265827591,0.0735810373368519,
0.0533));
#57659=CARTESIAN_POINT('Ctrl Pts',(0.355398841269737,0.0685119146864081,
0.0533));
#57660=CARTESIAN_POINT('Ctrl Pts',(0.355894985776107,0.0634376947345237,
0.0533));
#57661=CARTESIAN_POINT('Ctrl Pts',(0.356277894215268,0.05836243273793,0.0533));
#57662=CARTESIAN_POINT('Ctrl Pts',(0.357324187933274,0.0444943269424352,
0.0533));
#57663=CARTESIAN_POINT('Ctrl Pts',(0.357526229414497,0.0306157185946321,
0.0533));
#57664=CARTESIAN_POINT('Ctrl Pts',(0.356841349994185,0.0167882255892583,
0.0533));
#57665=CARTESIAN_POINT('Ctrl Pts',(0.355823943567287,-0.00375287965396633,
0.0533));
#57666=CARTESIAN_POINT('Ctrl Pts',(0.352851156603884,-0.0241829177690499,
0.0533));
#57667=CARTESIAN_POINT('Ctrl Pts',(0.348040392606845,-0.0442816943231375,
0.0533));
#57668=CARTESIAN_POINT('Ctrl Pts',(0.346677645286907,-0.0499750839593708,
0.0533));
#57669=CARTESIAN_POINT('Ctrl Pts',(0.345167119967579,-0.0556417158423305,
0.0533000000000001));
#57670=CARTESIAN_POINT('Ctrl Pts',(0.343510841709222,-0.0612760897393585,
0.0533000000000001));
#57671=CARTESIAN_POINT('Ctrl Pts',(0.342016897594177,-0.0663582307883981,
0.0533000000000001));
#57672=CARTESIAN_POINT('Ctrl Pts',(0.340406836566637,-0.0714055112317436,
0.0533));
#57673=CARTESIAN_POINT('Ctrl Pts',(0.338684647603792,-0.0764102645429386,
0.0533));
#57674=CARTESIAN_POINT('Ctrl Pts',(0.332034323863772,-0.0957363840782725,
0.0533));
#57675=CARTESIAN_POINT('Ctrl Pts',(0.323709882928168,-0.114451208546047,
0.0533));
#57676=CARTESIAN_POINT('Ctrl Pts',(0.313836238571883,-0.13233991066745,
0.0533));
#57677=CARTESIAN_POINT('Ctrl Pts',(0.305752963403788,-0.14698488839093,
0.0533));
#57678=CARTESIAN_POINT('Ctrl Pts',(0.296630038821398,-0.161076128885772,
0.0533));
#57679=CARTESIAN_POINT('Ctrl Pts',(0.286516038219096,-0.174473672389921,
0.0533));
#57680=CARTESIAN_POINT('Ctrl Pts',(0.283304266742829,-0.178728155830319,
0.0533000000000001));
#57681=CARTESIAN_POINT('Ctrl Pts',(0.279991464896629,-0.182913345906162,
0.0533000000000001));
#57682=CARTESIAN_POINT('Ctrl Pts',(0.27659067946394,-0.187011031331933,
0.0533000000000001));
#57683=CARTESIAN_POINT('Ctrl Pts',(0.264023874271964,-0.20215306704777,
0.0533000000000001));
#57684=CARTESIAN_POINT('Ctrl Pts',(0.250225650942623,-0.216149152210811,
0.0533000000000001));
#57685=CARTESIAN_POINT('Ctrl Pts',(0.235292709668539,-0.228787207872994,
0.0533000000000001));
#57686=CARTESIAN_POINT('Ctrl Pts',(0.221444282279375,-0.240507417104762,
0.0533000000000001));
#57687=CARTESIAN_POINT('Ctrl Pts',(0.206618876313766,-0.251060092225123,
0.0533));
#57688=CARTESIAN_POINT('Ctrl Pts',(0.190874522418597,-0.260231075837034,
0.0533));
#57689=CARTESIAN_POINT('Ctrl Pts',(0.189641532568663,-0.260949284395015,
0.0533));
#57690=CARTESIAN_POINT('Ctrl Pts',(0.188402901061074,-0.261658992964495,
0.0533));
#57691=CARTESIAN_POINT('Ctrl Pts',(0.187158653173906,-0.262360084935055,
0.0533));
#57692=CARTESIAN_POINT('Origin',(0.,0.,0.0533));
#57693=CARTESIAN_POINT('Origin',(0.,0.,-0.177777344927309));
#57694=CARTESIAN_POINT('Ctrl Pts',(0.187158653173902,-0.262360084935059,
0.0532999999999997));
#57695=CARTESIAN_POINT('Ctrl Pts',(0.274475898331453,-0.200070968026944,
0.0599211344550708));
#57696=CARTESIAN_POINT('Ctrl Pts',(0.380505034319934,0.0174746478065457,
0.0731634033652129));
#57697=CARTESIAN_POINT('Ctrl Pts',(0.191046375307344,0.329958431462181,
0.0930268067304262));
#57698=CARTESIAN_POINT('Ctrl Pts',(-0.173733796622045,0.338991571911486,
0.11289021009564));
#57699=CARTESIAN_POINT('Ctrl Pts',(-0.31746347429697,0.128188891668771,
0.126788826209727));
#57700=CARTESIAN_POINT('Ctrl Pts',(-0.322744636658635,0.0107979212988577,
0.134066307868744));
#57701=CARTESIAN_POINT('Ctrl Pts',(-0.322672883777213,0.000203620636067221,
0.13472265507269));
#57702=CARTESIAN_POINT('Ctrl Pts',(0.22840585926086,-0.320180657528383,
0.0122936971308065));
#57703=CARTESIAN_POINT('Ctrl Pts',(0.334966630404962,-0.244163871615853,
0.0189148315858776));
#57704=CARTESIAN_POINT('Ctrl Pts',(0.464363137066263,0.0213258210606221,
0.0321571004960198));
#57705=CARTESIAN_POINT('Ctrl Pts',(0.23315038215307,0.402676754616631,0.052020503861233));
#57706=CARTESIAN_POINT('Ctrl Pts',(-0.212022348030248,0.413700675611787,
0.0718839072264463));
#57707=CARTESIAN_POINT('Ctrl Pts',(-0.462705925125873,0.0460329065091048,
0.0917473105916596));
#57708=CARTESIAN_POINT('Ctrl Pts',(-0.289249672288166,-0.364136268728332,
0.111610713956873));
#57709=CARTESIAN_POINT('Ctrl Pts',(0.14941461449446,-0.440317672487742,
0.131474117322086));
#57710=CARTESIAN_POINT('Ctrl Pts',(0.451083062083358,-0.112907133063045,
0.151337520687299));
#57711=CARTESIAN_POINT('Ctrl Pts',(0.33921710497643,0.318056509301725,0.171200924052513));
#57712=CARTESIAN_POINT('Ctrl Pts',(-0.0836397209497935,0.457411044844623,
0.191064327417726));
#57713=CARTESIAN_POINT('Ctrl Pts',(-0.429815290904552,0.177433063463184,
0.210927730782939));
#57714=CARTESIAN_POINT('Ctrl Pts',(-0.38194714237817,-0.265217541271947,
0.230791134148153));
#57715=CARTESIAN_POINT('Ctrl Pts',(0.0160820867132626,-0.46471958682769,
0.250654537513365));
#57716=CARTESIAN_POINT('Ctrl Pts',(0.399367303186648,-0.238178907900465,
0.270517940878579));
#57717=CARTESIAN_POINT('Ctrl Pts',(0.416521813498203,0.206719639214314,
0.290381344243792));
#57718=CARTESIAN_POINT('Ctrl Pts',(0.0518184975661857,0.462101870037031,
0.310244747609006));
#57719=CARTESIAN_POINT('Ctrl Pts',(-0.360390794541395,0.293839833855819,
0.330108150974218));
#57720=CARTESIAN_POINT('Ctrl Pts',(-0.442202014837683,-0.143808009927119,
0.349971554339432));
#57721=CARTESIAN_POINT('Ctrl Pts',(-0.118612458427808,-0.449615872942682,
0.369834957704645));
#57722=CARTESIAN_POINT('Ctrl Pts',(0.313718299585274,-0.343226147934731,
0.389698361069858));
#57723=CARTESIAN_POINT('Ctrl Pts',(0.458439248795996,0.0778255316871185,
0.409561764435072));
#57724=CARTESIAN_POINT('Ctrl Pts',(0.182873504606443,0.427528522373788,
0.429425167800285));
#57725=CARTESIAN_POINT('Ctrl Pts',(-0.260346514431703,0.385283078075547,
0.449288571165498));
#57726=CARTESIAN_POINT('Ctrl Pts',(-0.464886762270973,-0.0101811444492372,
0.469151974530712));
#57727=CARTESIAN_POINT('Ctrl Pts',(-0.243229384295824,-0.39631152369195,
0.489015377895925));
#57728=CARTESIAN_POINT('Ctrl Pts',(0.201415169066835,-0.419112499346427,
0.508878781261138));
#57729=CARTESIAN_POINT('Ctrl Pts',(0.461406869855159,-0.0576806537548328,
0.528742184626351));
#57730=CARTESIAN_POINT('Ctrl Pts',(0.298391231378055,0.356631505027496,
0.548605587991565));
#57731=CARTESIAN_POINT('Ctrl Pts',(-0.138182711217647,0.443991999585549,
0.568468991356778));
#57732=CARTESIAN_POINT('Ctrl Pts',(-0.448073882458741,0.124310712416823,
0.588332394721992));
#57733=CARTESIAN_POINT('Ctrl Pts',(-0.347181094503187,-0.309335812638073,
0.608195798087204));
#57734=CARTESIAN_POINT('Ctrl Pts',(0.0719994360289554,-0.459390290033479,
0.628059201452418));
#57735=CARTESIAN_POINT('Ctrl Pts',(0.425172518796839,-0.188286182773711,
0.64792260481763));
#57736=CARTESIAN_POINT('Ctrl Pts',(0.38855709246268,0.255434420664781,0.667786008182846));
#57737=CARTESIAN_POINT('Ctrl Pts',(-0.0042786516855454,0.464978548433987,
0.687649411548056));
#57738=CARTESIAN_POINT('Ctrl Pts',(-0.393191825141502,0.248240903167881,
0.707512814913272));
#57739=CARTESIAN_POINT('Ctrl Pts',(-0.42163566312281,-0.196078364300367,
0.727376218278484));
#57740=CARTESIAN_POINT('Ctrl Pts',(-0.0635335009589411,-0.460637440531813,
0.747239621643697));
#57741=CARTESIAN_POINT('Ctrl Pts',(0.352814731969012,-0.302894572862218,
0.76710302500891));
#57742=CARTESIAN_POINT('Ctrl Pts',(0.445710431435121,0.132535160141284,
0.786966428374124));
#57743=CARTESIAN_POINT('Ctrl Pts',(0.129988929931527,0.446459668345332,
0.806829831739337));
#57744=CARTESIAN_POINT('Ctrl Pts',(-0.304903470342924,0.351080092196355,
0.826693235104551));
#57745=CARTESIAN_POINT('Ctrl Pts',(-0.460267293697333,-0.0661617390664321,
0.846556638469763));
#57746=CARTESIAN_POINT('Ctrl Pts',(-0.193668515362254,-0.422747990558374,
0.866420041834978));
#57747=CARTESIAN_POINT('Ctrl Pts',(0.250481159433732,-0.391768485374328,
0.886283445200189));
#57748=CARTESIAN_POINT('Ctrl Pts',(0.464995395961188,-0.00162453028868252,
0.906146848565404));
#57749=CARTESIAN_POINT('Ctrl Pts',(0.253212414024016,0.390008757270772,
0.926010251930616));
#57750=CARTESIAN_POINT('Ctrl Pts',(-0.190709958360289,0.424090873688623,
0.94587365529583));
#57751=CARTESIAN_POINT('Ctrl Pts',(-0.45979377215103,0.0693761086750143,
0.965737058661043));
#57752=CARTESIAN_POINT('Ctrl Pts',(-0.307349098051745,-0.348941097164749,
0.985600462026257));
#57753=CARTESIAN_POINT('Ctrl Pts',(0.126866248908158,-0.447357029956768,
1.00546386539147));
#57754=CARTESIAN_POINT('Ctrl Pts',(0.444773500139936,-0.135646197650459,
1.02532726875668));
#57755=CARTESIAN_POINT('Ctrl Pts',(0.354922507734706,0.30042198798866,1.0451906721219));
#57756=CARTESIAN_POINT('Ctrl Pts',(-0.0603133790844696,0.461070117950852,
1.06505407548711));
#57757=CARTESIAN_POINT('Ctrl Pts',(-0.420255329741598,0.199019635180803,
1.08491747885232));
#57758=CARTESIAN_POINT('Ctrl Pts',(-0.394916738548566,-0.245487529169761,
1.10478088221754));
#57759=CARTESIAN_POINT('Ctrl Pts',(-0.00752745044395922,-0.464937302067533,
1.12464428558275));
#57760=CARTESIAN_POINT('Ctrl Pts',(0.386762833270873,-0.25814311566201,
1.14450768894796));
#57761=CARTESIAN_POINT('Ctrl Pts',(0.426477735249094,0.18531081646884,1.16437109231318));
#57762=CARTESIAN_POINT('Ctrl Pts',(0.0752075353247572,0.458876000675463,
1.18423449567839));
#57763=CARTESIAN_POINT('Ctrl Pts',(-0.345011224938844,0.311754089030257,
1.2040978990436));
#57764=CARTESIAN_POINT('Ctrl Pts',(-0.448931529762247,-0.121176891149078,
1.22396130240882));
#57765=CARTESIAN_POINT('Ctrl Pts',(-0.141281603819434,-0.44301564960805,
1.24382470577403));
#57766=CARTESIAN_POINT('Ctrl Pts',(0.295892087836421,-0.358707721825574,
1.26368810913924));
#57767=CARTESIAN_POINT('Ctrl Pts',(0.46179863341371,0.0544552985883825,
1.28355151250445));
#57768=CARTESIAN_POINT('Ctrl Pts',(0.204338679793737,0.417694938177113,
1.30341491586967));
#57769=CARTESIAN_POINT('Ctrl Pts',(-0.240454334641303,0.398001344404975,
1.32327831923488));
#57770=CARTESIAN_POINT('Ctrl Pts',(-0.464804276183042,0.0134291577934678,
1.3431417226001));
#57771=CARTESIAN_POINT('Ctrl Pts',(-0.26303221329135,-0.383454576969892,
1.36300512596531));
#57772=CARTESIAN_POINT('Ctrl Pts',(0.179881808535696,-0.428795861789832,
1.38286852933052));
#57773=CARTESIAN_POINT('Ctrl Pts',(0.457884274494346,-0.0810268436371889,
1.40273193269574));
#57774=CARTESIAN_POINT('Ctrl Pts',(0.316108834951241,0.341025753553244,
1.42259533606095));
#57775=CARTESIAN_POINT('Ctrl Pts',(-0.115468002046529,0.450433667702228,
1.44245873942616));
#57776=CARTESIAN_POINT('Ctrl Pts',(-0.441186403406519,0.146894258209524,
1.46232214279137));
#57777=CARTESIAN_POINT('Ctrl Pts',(-0.362435117997404,-0.291314534468849,
1.48218554615659));
#57778=CARTESIAN_POINT('Ctrl Pts',(0.0485884293871068,-0.462452656508136,
1.5020489495218));
#57779=CARTESIAN_POINT('Ctrl Pts',(0.415067252117864,-0.209624918786039,
1.52191235288702));
#57780=CARTESIAN_POINT('Ctrl Pts',(0.401021760561521,0.235382630156459,
1.54177575625222));
#57781=CARTESIAN_POINT('Ctrl Pts',(0.0193287879203514,0.464595873692269,
1.56163915961744));
#57782=CARTESIAN_POINT('Ctrl Pts',(-0.380084687813499,0.267879812339231,
1.58150256298265));
#57783=CARTESIAN_POINT('Ctrl Pts',(-0.431044560988702,-0.174425522064151,
1.60136596634787));
#57784=CARTESIAN_POINT('Ctrl Pts',(-0.0868337066926223,-0.456815470675444,
1.62122936971308));
#57785=CARTESIAN_POINT('Ctrl Pts',(0.336986496472692,-0.320418926739431,
1.64109277307829));
#57786=CARTESIAN_POINT('Ctrl Pts',(0.451860956715713,0.109752564393622,
1.66095617644351));
#57787=CARTESIAN_POINT('Ctrl Pts',(0.152487559617347,0.439262932526176,
1.68081957980872));
#57788=CARTESIAN_POINT('Ctrl Pts',(-0.286698314532727,0.366148428326951,
1.70068298317393));
#57789=CARTESIAN_POINT('Ctrl Pts',(-0.463016271706304,-0.0427987589009261,
1.72054638653915));
#57790=CARTESIAN_POINT('Ctrl Pts',(-0.214907786272786,-0.41220913195275,
1.74040978990436));
#57791=CARTESIAN_POINT('Ctrl Pts',(0.230331103324425,-0.404295995834807,
1.76027319326957));
#57792=CARTESIAN_POINT('Ctrl Pts',(0.464202793554047,-0.0245699036739876,
1.78013659663479));
#57793=CARTESIAN_POINT('Ctrl Pts',(0.336664478059399,0.241817428859645,
1.79337886554493));
#57794=CARTESIAN_POINT('Ctrl Pts',(0.230637453473697,0.318576921724045,
1.8));
#57795=CARTESIAN_POINT('Ctrl Pts',(0.214656790565208,-0.300907133330608,
0.0259624647538709));
#57796=CARTESIAN_POINT('Ctrl Pts',(0.314803053047126,-0.229466237086217,
0.032583599208942));
#57797=CARTESIAN_POINT('Ctrl Pts',(0.43641043615082,0.0200420966425965,
0.0458258681190842));
#57798=CARTESIAN_POINT('Ctrl Pts',(0.219115713204495,0.378437313565148,
0.0656892714842974));
#57799=CARTESIAN_POINT('Ctrl Pts',(-0.199259497560847,0.38879764104502,
0.0855526748495107));
#57800=CARTESIAN_POINT('Ctrl Pts',(-0.434852981374653,0.0432619198281897,
0.105416078214724));
#57801=CARTESIAN_POINT('Ctrl Pts',(-0.271838062851545,-0.342216802259624,
0.125279481579937));
#57802=CARTESIAN_POINT('Ctrl Pts',(0.140420485335661,-0.413812407051313,
0.145142884945151));
#57803=CARTESIAN_POINT('Ctrl Pts',(0.423929765630718,-0.106110600199408,
0.165006288310364));
#57804=CARTESIAN_POINT('Ctrl Pts',(0.318797666989352,0.298910849861812,
0.184869691675577));
#57805=CARTESIAN_POINT('Ctrl Pts',(-0.0786049627665092,0.429876830538249,
0.20473309504079));
#57806=CARTESIAN_POINT('Ctrl Pts',(-0.403942224512066,0.166752341933838,
0.224596498406004));
#57807=CARTESIAN_POINT('Ctrl Pts',(-0.358955536490034,-0.24925256469017,
0.244459901771217));
#57808=CARTESIAN_POINT('Ctrl Pts',(0.0151140129707359,-0.436745429141075,
0.26432330513643));
#57809=CARTESIAN_POINT('Ctrl Pts',(0.37532707714306,-0.223841542925779,
0.284186708501643));
#57810=CARTESIAN_POINT('Ctrl Pts',(0.391448958337841,0.194275989434508,
0.304050111866857));
#57811=CARTESIAN_POINT('Ctrl Pts',(0.0486992427228591,0.434285287852625,
0.323913515232069));
#57812=CARTESIAN_POINT('Ctrl Pts',(-0.33869678981023,0.276151916066506,
0.343776918597283));
#57813=CARTESIAN_POINT('Ctrl Pts',(-0.415583319945026,-0.135151374699497,
0.363640321962496));
#57814=CARTESIAN_POINT('Ctrl Pts',(-0.111472489057659,-0.422550895083751,
0.38350372532771));
#57815=CARTESIAN_POINT('Ctrl Pts',(0.294833782060024,-0.322565382482518,
0.403367128692922));
#57816=CARTESIAN_POINT('Ctrl Pts',(0.430843140951487,0.0731407631575176,
0.423230532058136));
#57817=CARTESIAN_POINT('Ctrl Pts',(0.171865291482725,0.401793109795098,
0.443093935423349));
#57818=CARTESIAN_POINT('Ctrl Pts',(-0.244674753106583,0.362090662938401,
0.462957338788563));
#57819=CARTESIAN_POINT('Ctrl Pts',(-0.436902541328269,-0.00956828252491728,
0.482820742153776));
#57820=CARTESIAN_POINT('Ctrl Pts',(-0.228588001958665,-0.372455242676424,
0.502684145518989));
#57821=CARTESIAN_POINT('Ctrl Pts',(0.189290826001347,-0.393883695832501,
0.522547548884203));
#57822=CARTESIAN_POINT('Ctrl Pts',(0.433632123748318,-0.0542085218513332,
0.542410952249415));
#57823=CARTESIAN_POINT('Ctrl Pts',(0.280429338667971,0.335163793658248,
0.56227435561463));
#57824=CARTESIAN_POINT('Ctrl Pts',(-0.129864695229655,0.417265555166052,
0.582137758979841));
#57825=CARTESIAN_POINT('Ctrl Pts',(-0.421101725918668,0.116827732207138,
0.602001162345057));
#57826=CARTESIAN_POINT('Ctrl Pts',(-0.326282257960183,-0.290715102329896,
0.621864565710268));
#57827=CARTESIAN_POINT('Ctrl Pts',(0.0676653738677941,-0.43173693352053,
0.641727969075482));
#57828=CARTESIAN_POINT('Ctrl Pts',(0.399578927689504,-0.176952149269596,
0.661591372440696));
#57829=CARTESIAN_POINT('Ctrl Pts',(0.365167595478051,0.240058346651971,
0.681454775805909));
#57830=CARTESIAN_POINT('Ctrl Pts',(-0.00402109491296832,0.436988802351671,
0.701318179171121));
#57831=CARTESIAN_POINT('Ctrl Pts',(-0.369523336811412,0.233297848546726,
0.721181582536336));
#57832=CARTESIAN_POINT('Ctrl Pts',(-0.396254975799055,-0.184275274356786,
0.741044985901549));
#57833=CARTESIAN_POINT('Ctrl Pts',(-0.0597090523568472,-0.432909010822709,
0.760908389266761));
#57834=CARTESIAN_POINT('Ctrl Pts',(0.331576774228443,-0.284661598002026,
0.780771792631975));
#57835=CARTESIAN_POINT('Ctrl Pts',(0.418880544671259,0.12455710289149,0.800635195997188));
#57836=CARTESIAN_POINT('Ctrl Pts',(0.12216414499349,0.419584680681779,0.820498599362401));
#57837=CARTESIAN_POINT('Ctrl Pts',(-0.286549568333344,0.329946552448709,
0.840362002727615));
#57838=CARTESIAN_POINT('Ctrl Pts',(-0.432561145265387,-0.0621790816232671,
0.860225406092828));
#57839=CARTESIAN_POINT('Ctrl Pts',(-0.182010488153502,-0.397300345817796,
0.880088809458042));
#57840=CARTESIAN_POINT('Ctrl Pts',(0.235403250840818,-0.368185676090734,
0.899952212823254));
#57841=CARTESIAN_POINT('Ctrl Pts',(0.437004635728844,-0.00152674042195095,
0.919815616188469));
#57842=CARTESIAN_POINT('Ctrl Pts',(0.23797009543256,0.366531876191735,0.93967901955368));
#57843=CARTESIAN_POINT('Ctrl Pts',(-0.179230023795887,0.398562393051505,
0.959542422918895));
#57844=CARTESIAN_POINT('Ctrl Pts',(-0.432116127717582,0.0651999597482869,
0.979405826284106));
#57845=CARTESIAN_POINT('Ctrl Pts',(-0.288847979576343,-0.327936315889959,
0.999269229649322));
#57846=CARTESIAN_POINT('Ctrl Pts',(0.119229436187843,-0.420428024911697,
1.01913263301453));
#57847=CARTESIAN_POINT('Ctrl Pts',(0.418000012685543,-0.127480869073353,
1.03899603637975));
#57848=CARTESIAN_POINT('Ctrl Pts',(0.333557670789321,0.282337852301828,
1.05885943974496));
#57849=CARTESIAN_POINT('Ctrl Pts',(-0.0566827682280645,0.433315642887322,
1.07872284311017));
#57850=CARTESIAN_POINT('Ctrl Pts',(-0.394957732661426,0.187039493144428,
1.09858624647539));
#57851=CARTESIAN_POINT('Ctrl Pts',(-0.371144417711704,-0.23071021604214,
1.1184496498406));
#57852=CARTESIAN_POINT('Ctrl Pts',(-0.00707432969831571,-0.43695003884239,
1.13831305320581));
#57853=CARTESIAN_POINT('Ctrl Pts',(0.36348134311657,-0.242603989642943,
1.15817645657103));
#57854=CARTESIAN_POINT('Ctrl Pts',(0.400805575620254,0.174155887458163,
1.17803985993624));
#57855=CARTESIAN_POINT('Ctrl Pts',(0.0706803591263985,0.431253602211208,
1.19790326330145));
#57856=CARTESIAN_POINT('Ctrl Pts',(-0.324243005385255,0.292987808690079,
1.21776666666667));
#57857=CARTESIAN_POINT('Ctrl Pts',(-0.421907746474372,-0.113882553752806,
1.23763007003188));
#57858=CARTESIAN_POINT('Ctrl Pts',(-0.132777047576297,-0.416347977336323,
1.2574934733971));
#57859=CARTESIAN_POINT('Ctrl Pts',(0.27808063301942,-0.337115030968159,
1.27735687676231));
#57860=CARTESIAN_POINT('Ctrl Pts',(0.434000304794158,0.0511773194526611,
1.29722028012752));
#57861=CARTESIAN_POINT('Ctrl Pts',(0.192038353721738,0.392551465862486,
1.31708368349273));
#57862=CARTESIAN_POINT('Ctrl Pts',(-0.225979998580708,0.374043343314743,
1.33694708685795));
#57863=CARTESIAN_POINT('Ctrl Pts',(-0.436825020554684,0.0126207791747009,
1.35681049022316));
#57864=CARTESIAN_POINT('Ctrl Pts',(-0.247198784230396,-0.360372229881762,
1.37667389358837));
#57865=CARTESIAN_POINT('Ctrl Pts',(0.169053682888399,-0.402984160727349,
1.39653729695359));
#57866=CARTESIAN_POINT('Ctrl Pts',(0.430321573760419,-0.0761493696399576,
1.4164007003188));
#57867=CARTESIAN_POINT('Ctrl Pts',(0.297080417286682,0.320497442555603,
1.43626410368401));
#57868=CARTESIAN_POINT('Ctrl Pts',(-0.108517315678742,0.423319462050434,
1.45612750704923));
#57869=CARTESIAN_POINT('Ctrl Pts',(-0.41462884403543,0.138051843861415,
1.47599091041444));
#57870=CARTESIAN_POINT('Ctrl Pts',(-0.340618053622654,-0.273778629044111,
1.49585431377965));
#57871=CARTESIAN_POINT('Ctrl Pts',(0.0456636110150272,-0.434614958458733,
1.51571771714486));
#57872=CARTESIAN_POINT('Ctrl Pts',(0.390081955413338,-0.197006383438314,
1.53558112051008));
#57873=CARTESIAN_POINT('Ctrl Pts',(0.376881943166925,0.221213589299725,
1.55544452387529));
#57874=CARTESIAN_POINT('Ctrl Pts',(0.0181652764684949,0.436629163014252,
1.57530792724051));
#57875=CARTESIAN_POINT('Ctrl Pts',(-0.357205193829303,0.251754578275839,
1.59517133060572));
#57876=CARTESIAN_POINT('Ctrl Pts',(-0.405097497725524,-0.163925841833111,
1.61503473397093));
#57877=CARTESIAN_POINT('Ctrl Pts',(-0.0816066840484612,-0.429317107420319,
1.63489813733615));
#57878=CARTESIAN_POINT('Ctrl Pts',(0.316701331702821,-0.301131059740813,
1.65476154070136));
#57879=CARTESIAN_POINT('Ctrl Pts',(0.424660834289461,0.103145923249411,
1.67462494406657));
#57880=CARTESIAN_POINT('Ctrl Pts',(0.143308452132116,0.412821157983697,
1.69448834743178));
#57881=CARTESIAN_POINT('Ctrl Pts',(-0.26944028606448,0.344107838343119,
1.714351750797));
#57882=CARTESIAN_POINT('Ctrl Pts',(-0.43514464640082,-0.0402224542556716,
1.73421515416221));
#57883=CARTESIAN_POINT('Ctrl Pts',(-0.20197124459974,-0.387395882018906,
1.75407855752743));
#57884=CARTESIAN_POINT('Ctrl Pts',(0.216466143062017,-0.379959083296314,
1.77394196089264));
#57885=CARTESIAN_POINT('Ctrl Pts',(0.436259744641278,-0.0230908991749218,
1.79380536425785));
#57886=CARTESIAN_POINT('Ctrl Pts',(0.316398697438863,0.227261040280313,
1.80704763316799));
#57887=CARTESIAN_POINT('Ctrl Pts',(0.21675405222531,0.299399935652811,1.81366876762306));
#57888=CARTESIAN_POINT('Ctrl Pts',(0.200907721869555,-0.281633609132834,
0.0396312323769353));
#57889=CARTESIAN_POINT('Ctrl Pts',(0.294639475689289,-0.21476860255658,
0.0462523668320064));
#57890=CARTESIAN_POINT('Ctrl Pts',(0.408457735235377,0.0187583722245711,
0.0594946357421486));
#57891=CARTESIAN_POINT('Ctrl Pts',(0.20508104425592,0.354197872513664,0.0793580391073618));
#57892=CARTESIAN_POINT('Ctrl Pts',(-0.186496647091446,0.363894606478253,
0.0992214424725751));
#57893=CARTESIAN_POINT('Ctrl Pts',(-0.407000037623433,0.0404909331472749,
0.119084845837788));
#57894=CARTESIAN_POINT('Ctrl Pts',(-0.254426453414924,-0.320297335790916,
0.138948249203002));
#57895=CARTESIAN_POINT('Ctrl Pts',(0.131426356176862,-0.387307141614884,
0.158811652568215));
#57896=CARTESIAN_POINT('Ctrl Pts',(0.396776469178078,-0.0993140673357709,
0.178675055933428));
#57897=CARTESIAN_POINT('Ctrl Pts',(0.298378229002275,0.279765190421899,
0.198538459298642));
#57898=CARTESIAN_POINT('Ctrl Pts',(-0.0735702045832253,0.402342616231877,
0.218401862663855));
#57899=CARTESIAN_POINT('Ctrl Pts',(-0.378069158119579,0.156071620404493,
0.238265266029068));
#57900=CARTESIAN_POINT('Ctrl Pts',(-0.335963930601898,-0.233287588108394,
0.258128669394281));
#57901=CARTESIAN_POINT('Ctrl Pts',(0.0141459392282093,-0.408771271454461,
0.277992072759494));
#57902=CARTESIAN_POINT('Ctrl Pts',(0.351286851099471,-0.209504177951092,
0.297855476124708));
#57903=CARTESIAN_POINT('Ctrl Pts',(0.36637610317748,0.1818323396547,0.317718879489921));
#57904=CARTESIAN_POINT('Ctrl Pts',(0.0455799878795328,0.406468705668221,
0.337582282855134));
#57905=CARTESIAN_POINT('Ctrl Pts',(-0.317002785079066,0.258463998277192,
0.357445686220348));
#57906=CARTESIAN_POINT('Ctrl Pts',(-0.388964625052368,-0.126494739471875,
0.377309089585561));
#57907=CARTESIAN_POINT('Ctrl Pts',(-0.104332519687512,-0.395485917224819,
0.397172492950774));
#57908=CARTESIAN_POINT('Ctrl Pts',(0.275949264534774,-0.301904617030305,
0.417035896315987));
#57909=CARTESIAN_POINT('Ctrl Pts',(0.403247033106978,0.0684559946279179,
0.436899299681201));
#57910=CARTESIAN_POINT('Ctrl Pts',(0.160857078359007,0.376057697216407,
0.456762703046413));
#57911=CARTESIAN_POINT('Ctrl Pts',(-0.229002991781463,0.338898247801257,
0.476626106411628));
#57912=CARTESIAN_POINT('Ctrl Pts',(-0.408918320385565,-0.00895542060059796,
0.49648950977684));
#57913=CARTESIAN_POINT('Ctrl Pts',(-0.213946619621507,-0.348598961660897,
0.516352913142054));
#57914=CARTESIAN_POINT('Ctrl Pts',(0.177166482935859,-0.368654892318575,
0.536216316507268));
#57915=CARTESIAN_POINT('Ctrl Pts',(0.405857377641476,-0.0507363899478331,
0.556079719872479));
#57916=CARTESIAN_POINT('Ctrl Pts',(0.262467445957887,0.313696082288999,
0.575943123237694));
#57917=CARTESIAN_POINT('Ctrl Pts',(-0.121546679241664,0.390539110746556,
0.595806526602906));
#57918=CARTESIAN_POINT('Ctrl Pts',(-0.394129569378595,0.109344751997453,
0.61566992996812));
#57919=CARTESIAN_POINT('Ctrl Pts',(-0.305383421417179,-0.27209439202172,
0.635533333333333));
#57920=CARTESIAN_POINT('Ctrl Pts',(0.063331311706633,-0.404083577007581,
0.655396736698547));
#57921=CARTESIAN_POINT('Ctrl Pts',(0.373985336582169,-0.165618115765482,
0.67526014006376));
#57922=CARTESIAN_POINT('Ctrl Pts',(0.341778098493423,0.224682272639162,
0.695123543428973));
#57923=CARTESIAN_POINT('Ctrl Pts',(-0.00376353814039183,0.408999056269356,
0.714986946794187));
#57924=CARTESIAN_POINT('Ctrl Pts',(-0.345854848481321,0.218354793925571,
0.7348503501594));
#57925=CARTESIAN_POINT('Ctrl Pts',(-0.3708742884753,-0.172472184413205,
0.754713753524613));
#57926=CARTESIAN_POINT('Ctrl Pts',(-0.0558846037547525,-0.405180581113605,
0.774577156889825));
#57927=CARTESIAN_POINT('Ctrl Pts',(0.310338816487874,-0.266428623141834,
0.79444056025504));
#57928=CARTESIAN_POINT('Ctrl Pts',(0.392050657907398,0.116579045641696,
0.814303963620252));
#57929=CARTESIAN_POINT('Ctrl Pts',(0.114339360055454,0.392709693018225,
0.834167366985466));
#57930=CARTESIAN_POINT('Ctrl Pts',(-0.268195666323763,0.308813012701063,
0.85403077035068));
#57931=CARTESIAN_POINT('Ctrl Pts',(-0.404854996833441,-0.0581964241801013,
0.873894173715892));
#57932=CARTESIAN_POINT('Ctrl Pts',(-0.17035246094475,-0.371852701077219,
0.893757577081107));
#57933=CARTESIAN_POINT('Ctrl Pts',(0.220325342247905,-0.344602866807139,
0.913620980446318));
#57934=CARTESIAN_POINT('Ctrl Pts',(0.4090138754965,-0.00142895055522028,
0.933484383811533));
#57935=CARTESIAN_POINT('Ctrl Pts',(0.222727776841105,0.343054995112699,
0.953347787176745));
#57936=CARTESIAN_POINT('Ctrl Pts',(-0.167750089231486,0.373033912414387,
0.973211190541959));
#57937=CARTESIAN_POINT('Ctrl Pts',(-0.404438483284133,0.0610238108215602,
0.993074593907172));
#57938=CARTESIAN_POINT('Ctrl Pts',(-0.270346861100941,-0.306931534615169,
1.01293799727239));
#57939=CARTESIAN_POINT('Ctrl Pts',(0.111592623467528,-0.393499019866625,
1.0328014006376));
#57940=CARTESIAN_POINT('Ctrl Pts',(0.39122652523115,-0.119315540496249,
1.05266480400281));
#57941=CARTESIAN_POINT('Ctrl Pts',(0.312192833843937,0.264253716614997,
1.07252820736802));
#57942=CARTESIAN_POINT('Ctrl Pts',(-0.0530521573716599,0.405561167823791,
1.09239161073324));
#57943=CARTESIAN_POINT('Ctrl Pts',(-0.369660135581253,0.175059351108053,
1.11225501409845));
#57944=CARTESIAN_POINT('Ctrl Pts',(-0.347372096874843,-0.215932902914519,
1.13211841746366));
#57945=CARTESIAN_POINT('Ctrl Pts',(-0.00662120895267193,-0.408962775617247,
1.15198182082888));
#57946=CARTESIAN_POINT('Ctrl Pts',(0.340199852962266,-0.227064863623877,
1.17184522419409));
#57947=CARTESIAN_POINT('Ctrl Pts',(0.375133415991415,0.163000958447487,
1.1917086275593));
#57948=CARTESIAN_POINT('Ctrl Pts',(0.0661531829280398,0.403631203746953,
1.21157203092452));
#57949=CARTESIAN_POINT('Ctrl Pts',(-0.303474785831665,0.274221528349901,
1.23143543428973));
#57950=CARTESIAN_POINT('Ctrl Pts',(-0.394883963186496,-0.106588216356535,
1.25129883765494));
#57951=CARTESIAN_POINT('Ctrl Pts',(-0.124272491333159,-0.389680305064596,
1.27116224102016));
#57952=CARTESIAN_POINT('Ctrl Pts',(0.260269178202419,-0.315522340110745,
1.29102564438537));
#57953=CARTESIAN_POINT('Ctrl Pts',(0.406201976174607,0.0478993403169399,
1.31088904775058));
#57954=CARTESIAN_POINT('Ctrl Pts',(0.179738027649738,0.367407993547859,
1.3307524511158));
#57955=CARTESIAN_POINT('Ctrl Pts',(-0.211505662520113,0.350085342224511,
1.35061585448101));
#57956=CARTESIAN_POINT('Ctrl Pts',(-0.408845764926325,0.0118124005559338,
1.37047925784622));
#57957=CARTESIAN_POINT('Ctrl Pts',(-0.231365355169441,-0.337289882793632,
1.39034266121144));
#57958=CARTESIAN_POINT('Ctrl Pts',(0.158225557241102,-0.377172459664866,
1.41020606457665));
#57959=CARTESIAN_POINT('Ctrl Pts',(0.402758873026492,-0.0712718956427259,
1.43006946794187));
#57960=CARTESIAN_POINT('Ctrl Pts',(0.278051999622122,0.299969131557961,
1.44993287130708));
#57961=CARTESIAN_POINT('Ctrl Pts',(-0.101566629310955,0.39620525639864,
1.46979627467229));
#57962=CARTESIAN_POINT('Ctrl Pts',(-0.388071284664342,0.129209429513306,
1.4896596780375));
#57963=CARTESIAN_POINT('Ctrl Pts',(-0.318800989247905,-0.256242723619373,
1.50952308140272));
#57964=CARTESIAN_POINT('Ctrl Pts',(0.0427387926429474,-0.40677726040933,
1.52938648476793));
#57965=CARTESIAN_POINT('Ctrl Pts',(0.365096658708812,-0.184387848090589,
1.54924988813315));
#57966=CARTESIAN_POINT('Ctrl Pts',(0.35274212577233,0.207044548442991,1.56911329149835));
#57967=CARTESIAN_POINT('Ctrl Pts',(0.0170017650166384,0.408662452336233,
1.58897669486357));
#57968=CARTESIAN_POINT('Ctrl Pts',(-0.334325699845108,0.235629344212447,
1.60884009822878));
#57969=CARTESIAN_POINT('Ctrl Pts',(-0.379150434462346,-0.153426161602072,
1.628703501594));
#57970=CARTESIAN_POINT('Ctrl Pts',(-0.0763796614043001,-0.401818744165193,
1.64856690495921));
#57971=CARTESIAN_POINT('Ctrl Pts',(0.29641616693295,-0.281843192742194,
1.66843030832442));
#57972=CARTESIAN_POINT('Ctrl Pts',(0.397460711863209,0.0965392821051996,
1.68829371168964));
#57973=CARTESIAN_POINT('Ctrl Pts',(0.134129344646885,0.386379383441219,
1.70815711505485));
#57974=CARTESIAN_POINT('Ctrl Pts',(-0.252182257596233,0.322067248359287,
1.72802051842006));
#57975=CARTESIAN_POINT('Ctrl Pts',(-0.407273021095337,-0.0376461496104168,
1.74788392178527));
#57976=CARTESIAN_POINT('Ctrl Pts',(-0.189034702926694,-0.362582632085062,
1.76774732515049));
#57977=CARTESIAN_POINT('Ctrl Pts',(0.202601182799609,-0.35562217075782,
1.7876107285157));
#57978=CARTESIAN_POINT('Ctrl Pts',(0.408316695728509,-0.0216118946758564,
1.80747413188092));
#57979=CARTESIAN_POINT('Ctrl Pts',(0.296132916818328,0.21270465170098,1.82071640079106));
#57980=CARTESIAN_POINT('Ctrl Pts',(0.202870650976924,0.280222949581577,
1.82733753524613));
#57981=CARTESIAN_POINT('Ctrl Pts',(0.187158653173902,-0.262360084935059,
0.0532999999999997));
#57982=CARTESIAN_POINT('Ctrl Pts',(0.274475898331453,-0.200070968026944,
0.0599211344550708));
#57983=CARTESIAN_POINT('Ctrl Pts',(0.380505034319934,0.0174746478065457,
0.0731634033652129));
#57984=CARTESIAN_POINT('Ctrl Pts',(0.191046375307344,0.329958431462181,
0.0930268067304262));
#57985=CARTESIAN_POINT('Ctrl Pts',(-0.173733796622045,0.338991571911486,
0.11289021009564));
#57986=CARTESIAN_POINT('Ctrl Pts',(-0.379147093872213,0.0377199464663596,
0.132753613460853));
#57987=CARTESIAN_POINT('Ctrl Pts',(-0.237014843978304,-0.298377869322208,
0.152617016826066));
#57988=CARTESIAN_POINT('Ctrl Pts',(0.122432227018064,-0.360801876178455,
0.172480420191279));
#57989=CARTESIAN_POINT('Ctrl Pts',(0.369623172725438,-0.0925175344721341,
0.192343823556493));
#57990=CARTESIAN_POINT('Ctrl Pts',(0.277958791015197,0.260619530981986,
0.212207226921706));
#57991=CARTESIAN_POINT('Ctrl Pts',(-0.0685354463999416,0.374808401925503,
0.232070630286919));
#57992=CARTESIAN_POINT('Ctrl Pts',(-0.352196091727093,0.145390898875147,
0.251934033652132));
#57993=CARTESIAN_POINT('Ctrl Pts',(-0.312972324713763,-0.217322611526617,
0.271797437017346));
#57994=CARTESIAN_POINT('Ctrl Pts',(0.0131778654856828,-0.380797113767846,
0.291660840382558));
#57995=CARTESIAN_POINT('Ctrl Pts',(0.327246625055882,-0.195166812976406,
0.311524243747772));
#57996=CARTESIAN_POINT('Ctrl Pts',(0.341303248017118,0.169388689874893,
0.331387647112985));
#57997=CARTESIAN_POINT('Ctrl Pts',(0.0424607330362066,0.378652123483815,
0.351251050478199));
#57998=CARTESIAN_POINT('Ctrl Pts',(-0.295308780347901,0.240776080487878,
0.371114453843412));
#57999=CARTESIAN_POINT('Ctrl Pts',(-0.362345930159709,-0.117838104244253,
0.390977857208625));
#58000=CARTESIAN_POINT('Ctrl Pts',(-0.0971925503173641,-0.368420939365887,
0.410841260573839));
#58001=CARTESIAN_POINT('Ctrl Pts',(0.257064747009525,-0.281243851578092,
0.430704663939052));
#58002=CARTESIAN_POINT('Ctrl Pts',(0.375650925262469,0.063771226098318,
0.450568067304265));
#58003=CARTESIAN_POINT('Ctrl Pts',(0.149848865235289,0.350322284637716,
0.470431470669478));
#58004=CARTESIAN_POINT('Ctrl Pts',(-0.213331230456342,0.315705832664112,
0.490294874034692));
#58005=CARTESIAN_POINT('Ctrl Pts',(-0.380934099442862,-0.00834255867627857,
0.510158277399905));
#58006=CARTESIAN_POINT('Ctrl Pts',(-0.199305237284349,-0.324742680645371,
0.530021680765118));
#58007=CARTESIAN_POINT('Ctrl Pts',(0.16504213987037,-0.34342608880465,0.549885084130331));
#58008=CARTESIAN_POINT('Ctrl Pts',(0.378082631534635,-0.0472642580443332,
0.569748487495545));
#58009=CARTESIAN_POINT('Ctrl Pts',(0.244505553247802,0.29222837091975,0.589611890860758));
#58010=CARTESIAN_POINT('Ctrl Pts',(-0.113228663253673,0.363812666327059,
0.609475294225971));
#58011=CARTESIAN_POINT('Ctrl Pts',(-0.367157412838523,0.101861771787768,
0.629338697591184));
#58012=CARTESIAN_POINT('Ctrl Pts',(-0.284484584874175,-0.253473681713543,
0.649202100956398));
#58013=CARTESIAN_POINT('Ctrl Pts',(0.0589972495454716,-0.376430220494633,
0.66906550432161));
#58014=CARTESIAN_POINT('Ctrl Pts',(0.348391745474835,-0.154284082261366,
0.688928907686824));
#58015=CARTESIAN_POINT('Ctrl Pts',(0.318388601508794,0.209306198626352,
0.708792311052038));
#58016=CARTESIAN_POINT('Ctrl Pts',(-0.00350598136781482,0.381009310187041,
0.72865571441725));
#58017=CARTESIAN_POINT('Ctrl Pts',(-0.322186360151231,0.203411739304416,
0.748519117782465));
#58018=CARTESIAN_POINT('Ctrl Pts',(-0.345493601151545,-0.160669094469624,
0.768382521147676));
#58019=CARTESIAN_POINT('Ctrl Pts',(-0.0520601551526582,-0.377452151404502,
0.788245924512891));
#58020=CARTESIAN_POINT('Ctrl Pts',(0.289100858747305,-0.248195648281641,
0.808109327878104));
#58021=CARTESIAN_POINT('Ctrl Pts',(0.365220771143536,0.108600988391901,
0.827972731243317));
#58022=CARTESIAN_POINT('Ctrl Pts',(0.106514575117418,0.365834705354672,
0.84783613460853));
#58023=CARTESIAN_POINT('Ctrl Pts',(-0.249841764314182,0.287679472953417,
0.867699537973743));
#58024=CARTESIAN_POINT('Ctrl Pts',(-0.377148848401494,-0.0542137667369359,
0.887562941338957));
#58025=CARTESIAN_POINT('Ctrl Pts',(-0.158694433735999,-0.346405056336641,
0.90742634470417));
#58026=CARTESIAN_POINT('Ctrl Pts',(0.205247433654992,-0.321020057523545,
0.927289748069383));
#58027=CARTESIAN_POINT('Ctrl Pts',(0.381023115264154,-0.00133116068848917,
0.947153151434597));
#58028=CARTESIAN_POINT('Ctrl Pts',(0.207485458249651,0.319578114033663,
0.96701655479981));
#58029=CARTESIAN_POINT('Ctrl Pts',(-0.156270154667085,0.347505431777269,
0.986879958165023));
#58030=CARTESIAN_POINT('Ctrl Pts',(-0.376760838850683,0.0568476618948332,
1.00674336153024));
#58031=CARTESIAN_POINT('Ctrl Pts',(-0.251845742625539,-0.28592675334038,
1.02660676489545));
#58032=CARTESIAN_POINT('Ctrl Pts',(0.103955810747213,-0.366570014821552,
1.04647016826066));
#58033=CARTESIAN_POINT('Ctrl Pts',(0.364453037776757,-0.111150211919144,
1.06633357162588));
#58034=CARTESIAN_POINT('Ctrl Pts',(0.290827996898553,0.246169580928165,
1.08619697499109));
#58035=CARTESIAN_POINT('Ctrl Pts',(-0.0494215465152554,0.377806692760261,
1.1060603783563));
#58036=CARTESIAN_POINT('Ctrl Pts',(-0.34436253850108,0.163079209071679,
1.12592378172152));
#58037=CARTESIAN_POINT('Ctrl Pts',(-0.323599776037981,-0.201155589786898,
1.14578718508673));
#58038=CARTESIAN_POINT('Ctrl Pts',(-0.00616808820702852,-0.380975512392104,
1.16565058845194));
#58039=CARTESIAN_POINT('Ctrl Pts',(0.316918362807963,-0.211525737604811,
1.18551399181716));
#58040=CARTESIAN_POINT('Ctrl Pts',(0.349461256362576,0.151846029436811,
1.20537739518237));
#58041=CARTESIAN_POINT('Ctrl Pts',(0.0616260067296811,0.376008805282698,
1.22524079854758));
#58042=CARTESIAN_POINT('Ctrl Pts',(-0.282706566278076,0.255455248009724,
1.2451042019128));
#58043=CARTESIAN_POINT('Ctrl Pts',(-0.367860179898621,-0.0992938789602632,
1.26496760527801));
#58044=CARTESIAN_POINT('Ctrl Pts',(-0.115767935090022,-0.363012632792868,
1.28483100864322));
#58045=CARTESIAN_POINT('Ctrl Pts',(0.242457723385417,-0.293929649253331,
1.30469441200844));
#58046=CARTESIAN_POINT('Ctrl Pts',(0.378403647555055,0.0446213611812189,
1.32455781537365));
#58047=CARTESIAN_POINT('Ctrl Pts',(0.167437701577738,0.342264521233232,
1.34442121873886));
#58048=CARTESIAN_POINT('Ctrl Pts',(-0.197031326459517,0.326127341134279,
1.36428462210407));
#58049=CARTESIAN_POINT('Ctrl Pts',(-0.380866509297967,0.0110040219371662,
1.38414802546929));
#58050=CARTESIAN_POINT('Ctrl Pts',(-0.215531926108487,-0.314207535705501,
1.4040114288345));
#58051=CARTESIAN_POINT('Ctrl Pts',(0.147397431593805,-0.351360758602383,
1.42387483219971));
#58052=CARTESIAN_POINT('Ctrl Pts',(0.375196172292565,-0.0663944216454938,
1.44373823556493));
#58053=CARTESIAN_POINT('Ctrl Pts',(0.259023581957562,0.279440820560319,
1.46360163893014));
#58054=CARTESIAN_POINT('Ctrl Pts',(-0.0946159429431672,0.369091050746847,
1.48346504229536));
#58055=CARTESIAN_POINT('Ctrl Pts',(-0.361513725293254,0.120367015165197,
1.50332844566056));
#58056=CARTESIAN_POINT('Ctrl Pts',(-0.296983924873155,-0.238706818194636,
1.52319184902578));
#58057=CARTESIAN_POINT('Ctrl Pts',(0.039813974270868,-0.378939562359927,
1.54305525239099));
#58058=CARTESIAN_POINT('Ctrl Pts',(0.340111362004286,-0.171769312742865,
1.56291865575621));
#58059=CARTESIAN_POINT('Ctrl Pts',(0.328602308377735,0.192875507586258,
1.58278205912142));
#58060=CARTESIAN_POINT('Ctrl Pts',(0.0158382535647818,0.380695741658215,
1.60264546248663));
#58061=CARTESIAN_POINT('Ctrl Pts',(-0.311446205860912,0.219504110149056,
1.62250886585185));
#58062=CARTESIAN_POINT('Ctrl Pts',(-0.353203371199169,-0.142926481371032,
1.64237226921706));
#58063=CARTESIAN_POINT('Ctrl Pts',(-0.0711526387601384,-0.374320380910067,
1.66223567258227));
#58064=CARTESIAN_POINT('Ctrl Pts',(0.276131002163078,-0.262555325743576,
1.68209907594749));
#58065=CARTESIAN_POINT('Ctrl Pts',(0.370260589436959,0.089932640960989,
1.7019624793127));
#58066=CARTESIAN_POINT('Ctrl Pts',(0.124950237161653,0.359937608898739,
1.72182588267791));
#58067=CARTESIAN_POINT('Ctrl Pts',(-0.234924229127985,0.300026658375456,
1.74168928604313));
#58068=CARTESIAN_POINT('Ctrl Pts',(-0.379401395789853,-0.0350698449651625,
1.76155268940834));
#58069=CARTESIAN_POINT('Ctrl Pts',(-0.176098161253648,-0.337769382151217,
1.78141609277355));
#58070=CARTESIAN_POINT('Ctrl Pts',(0.188736222537201,-0.331285258219327,
1.80127949613877));
#58071=CARTESIAN_POINT('Ctrl Pts',(0.38037364681574,-0.0201328901767907,
1.82114289950398));
#58072=CARTESIAN_POINT('Ctrl Pts',(0.275867136197792,0.198148263121647,
1.83438516841412));
#58073=CARTESIAN_POINT('Ctrl Pts',(0.188987249728538,0.261045963510343,
1.84100630286919));
#58074=CARTESIAN_POINT('',(0.230637453473697,0.318576921724045,1.8));
#58075=CARTESIAN_POINT('Ctrl Pts',(0.141603157807409,-0.290105179958815,
1.8));
#58076=CARTESIAN_POINT('Ctrl Pts',(0.148157166114403,-0.287770754305551,
1.8));
#58077=CARTESIAN_POINT('Ctrl Pts',(0.154616475711889,-0.285214128338566,
1.8));
#58078=CARTESIAN_POINT('Ctrl Pts',(0.160969423134311,-0.282436150032975,
1.8));
#58079=CARTESIAN_POINT('Ctrl Pts',(0.177873482965308,-0.275044445306887,
1.8));
#58080=CARTESIAN_POINT('Ctrl Pts',(0.194025306149541,-0.266089662887484,
1.8));
#58081=CARTESIAN_POINT('Ctrl Pts',(0.209336262334518,-0.255787677754136,
1.8));
#58082=CARTESIAN_POINT('Ctrl Pts',(0.219828851204133,-0.248727733669706,
1.8));
#58083=CARTESIAN_POINT('Ctrl Pts',(0.229926482288665,-0.241033833322765,
1.8));
#58084=CARTESIAN_POINT('Ctrl Pts',(0.239596477203674,-0.232762290241159,
1.8));
#58085=CARTESIAN_POINT('Ctrl Pts',(0.243434784886035,-0.229479069553439,
1.8));
#58086=CARTESIAN_POINT('Ctrl Pts',(0.247207605954188,-0.226102903767889,
1.8));
#58087=CARTESIAN_POINT('Ctrl Pts',(0.250906256816858,-0.222642971761847,
1.8));
#58088=CARTESIAN_POINT('Ctrl Pts',(0.265338639470732,-0.209142086027652,
1.8));
#58089=CARTESIAN_POINT('Ctrl Pts',(0.278586410411045,-0.194425703806486,
1.8));
#58090=CARTESIAN_POINT('Ctrl Pts',(0.290546071531598,-0.178726454802016,
1.8));
#58091=CARTESIAN_POINT('Ctrl Pts',(0.299413028045636,-0.167086947894376,
1.8));
#58092=CARTESIAN_POINT('Ctrl Pts',(0.307571782002005,-0.154905816290907,
1.8));
#58093=CARTESIAN_POINT('Ctrl Pts',(0.314970614874736,-0.142261835016312,
1.8));
#58094=CARTESIAN_POINT('Ctrl Pts',(0.319430822453677,-0.134639716490457,
1.8));
#58095=CARTESIAN_POINT('Ctrl Pts',(0.323614695300392,-0.126849161122988,
1.8));
#58096=CARTESIAN_POINT('Ctrl Pts',(0.327508820353545,-0.118905724928063,
1.8));
#58097=CARTESIAN_POINT('Ctrl Pts',(0.329797917149386,-0.114236307769246,
1.8));
#58098=CARTESIAN_POINT('Ctrl Pts',(0.331983045551948,-0.109521668097398,
1.8));
#58099=CARTESIAN_POINT('Ctrl Pts',(0.334060558900541,-0.104769521658052,
1.8));
#58100=CARTESIAN_POINT('Ctrl Pts',(0.342241183697153,-0.0860569935170526,
1.8));
#58101=CARTESIAN_POINT('Ctrl Pts',(0.348765534562484,-0.066746552171421,
1.8));
#58102=CARTESIAN_POINT('Ctrl Pts',(0.353504988432865,-0.0470500087636206,
1.8));
#58103=CARTESIAN_POINT('Ctrl Pts',(0.355704075360087,-0.037910894362647,
1.8));
#58104=CARTESIAN_POINT('Ctrl Pts',(0.357518357519014,-0.0286881552166209,
1.8));
#58105=CARTESIAN_POINT('Ctrl Pts',(0.358931711772656,-0.0194009408651651,
1.8));
#58106=CARTESIAN_POINT('Ctrl Pts',(0.360583937406819,-0.00854409193157186,
1.8));
#58107=CARTESIAN_POINT('Ctrl Pts',(0.361688388824116,0.00240089241339821,
1.8));
#58108=CARTESIAN_POINT('Ctrl Pts',(0.362260654583105,0.0134037927651624,
1.8));
#58109=CARTESIAN_POINT('Ctrl Pts',(0.36252518757313,0.0184899438816373,
1.8));
#58110=CARTESIAN_POINT('Ctrl Pts',(0.362675431445883,0.0235795032329619,
1.8));
#58111=CARTESIAN_POINT('Ctrl Pts',(0.362713867593775,0.0286667428322311,
1.8));
#58112=CARTESIAN_POINT('Ctrl Pts',(0.362867054460235,0.0489418831852718,
1.8));
#58113=CARTESIAN_POINT('Ctrl Pts',(0.361248999287613,0.0691916862605563,
1.8));
#58114=CARTESIAN_POINT('Ctrl Pts',(0.357992028648484,0.0892225189703539,
1.8));
#58115=CARTESIAN_POINT('Ctrl Pts',(0.35587100389236,0.102267122920059,1.8));
#58116=CARTESIAN_POINT('Ctrl Pts',(0.353053837305762,0.115219322766376,
1.8));
#58117=CARTESIAN_POINT('Ctrl Pts',(0.349565738552542,0.128027375249902,
1.8));
#58118=CARTESIAN_POINT('Ctrl Pts',(0.34755041814521,0.135427489574188,1.8));
#58119=CARTESIAN_POINT('Ctrl Pts',(0.345310966761358,0.142779491872179,
1.8));
#58120=CARTESIAN_POINT('Ctrl Pts',(0.342850970118154,0.150073252099977,
1.8));
#58121=CARTESIAN_POINT('Ctrl Pts',(0.341081076039099,0.155320894643267,
1.8));
#58122=CARTESIAN_POINT('Ctrl Pts',(0.339197374240118,0.160536742001126,
1.8));
#58123=CARTESIAN_POINT('Ctrl Pts',(0.337205955025213,0.165705865160006,
1.8));
#58124=CARTESIAN_POINT('Ctrl Pts',(0.331562736590182,0.180353956774669,
1.8));
#58125=CARTESIAN_POINT('Ctrl Pts',(0.325047469011081,0.194651789699771,
1.8));
#58126=CARTESIAN_POINT('Ctrl Pts',(0.317704114220749,0.208516108946925,
1.8));
#58127=CARTESIAN_POINT('Ctrl Pts',(0.313549190673617,0.216360641609406,
1.8));
#58128=CARTESIAN_POINT('Ctrl Pts',(0.309128890575192,0.224066387719809,
1.8));
#58129=CARTESIAN_POINT('Ctrl Pts',(0.304449133391761,0.231617862092355,
1.8));
#58130=CARTESIAN_POINT('Ctrl Pts',(0.299771419854562,0.239166038742062,
1.8));
#58131=CARTESIAN_POINT('Ctrl Pts',(0.294831254196119,0.246563958455385,
1.8));
#58132=CARTESIAN_POINT('Ctrl Pts',(0.289651947072993,0.253771225125073,
1.8));
#58133=CARTESIAN_POINT('Ctrl Pts',(0.276941700269071,0.271458173586651,
1.8));
#58134=CARTESIAN_POINT('Ctrl Pts',(0.262780082335297,0.288025513613553,
1.8));
#58135=CARTESIAN_POINT('Ctrl Pts',(0.24725665255325,0.303250481813621,1.8));
#58136=CARTESIAN_POINT('Ctrl Pts',(0.24187988232453,0.308523875445098,1.8));
#58137=CARTESIAN_POINT('Ctrl Pts',(0.236339326786495,0.313636036829337,
1.8));
#58138=CARTESIAN_POINT('Ctrl Pts',(0.230637453473697,0.318576921724045,
1.8));
#58139=CARTESIAN_POINT('Ctrl Pts',(0.230637453473696,0.318576921724045,
1.8));
#58140=CARTESIAN_POINT('Ctrl Pts',(0.336664478059399,0.241817428859645,
1.79337886554493));
#58141=CARTESIAN_POINT('Ctrl Pts',(0.400433635806723,0.108623762592829,
1.78675773108986));
#58142=CARTESIAN_POINT('Ctrl Pts',(0.393339599642115,-0.0212607525673823,
1.78013659663479));
#58143=CARTESIAN_POINT('Ctrl Pts',(0.386245563477507,-0.151145267727593,
1.77351546217972));
#58144=CARTESIAN_POINT('Ctrl Pts',(0.308288333400966,-0.277720631781199,
1.76689432772464));
#58145=CARTESIAN_POINT('Ctrl Pts',(0.195103236763162,-0.34232716982766,
1.76027319326957));
#58146=CARTESIAN_POINT('Ctrl Pts',(0.0819181401253553,-0.406933707874121,
1.7536520588145));
#58147=CARTESIAN_POINT('Ctrl Pts',(-0.0664948230737163,-0.409571419913436,
1.74703092435943));
#58148=CARTESIAN_POINT('Ctrl Pts',(-0.182052718912172,-0.349321880424455,
1.74040978990436));
#58149=CARTESIAN_POINT('Ctrl Pts',(-0.297610614750626,-0.289072340935474,
1.73378865544929));
#58150=CARTESIAN_POINT('Ctrl Pts',(-0.380313443228465,-0.1659355499182,
1.72716752099422));
#58151=CARTESIAN_POINT('Ctrl Pts',(-0.392278531271789,-0.0362092898715836,
1.72054638653915));
#58152=CARTESIAN_POINT('Ctrl Pts',(-0.393380886268349,-0.0242574855530751,
1.71993637509393));
#58153=CARTESIAN_POINT('Ctrl Pts',(-0.393882811330762,-0.0122497490768379,
1.71932636364871));
#58154=CARTESIAN_POINT('Ctrl Pts',(-0.393805363403874,-0.000235004724456311,
1.7187163522035));
#58155=CARTESIAN_POINT('Origin',(0.275,0.,1.8));
#58156=CARTESIAN_POINT('Origin',(0.,0.,1.8));
#58157=CARTESIAN_POINT('',(-0.275,-3.36777869765522E-17,1.8));
#58158=CARTESIAN_POINT('Origin',(0.,0.,1.8));
#58159=CARTESIAN_POINT('Origin',(-0.115470053837925,-0.2,0.));
#58160=CARTESIAN_POINT('',(-0.115470053837925,-0.2,0.));
#58161=CARTESIAN_POINT('',(0.115470053837925,-0.2,0.));
#58162=CARTESIAN_POINT('',(0.112264973081037,-0.2,0.));
#58163=CARTESIAN_POINT('',(-0.115470053837925,-0.2,0.36));
#58164=CARTESIAN_POINT('',(-0.115470053837925,-0.2,0.));
#58165=CARTESIAN_POINT('',(0.115470053837925,-0.2,0.36));
#58166=CARTESIAN_POINT('',(-0.115470053837925,-0.2,0.36));
#58167=CARTESIAN_POINT('',(0.115470053837925,-0.2,0.));
#58168=CARTESIAN_POINT('Origin',(-0.23094010767585,2.82820063659975E-17,
0.));
#58169=CARTESIAN_POINT('',(-0.23094010767585,2.82820063659975E-17,0.));
#58170=CARTESIAN_POINT('',(-0.159572594216369,-0.123612159321677,0.));
#58171=CARTESIAN_POINT('',(-0.23094010767585,2.77555756156289E-17,0.36));
#58172=CARTESIAN_POINT('',(-0.23094010767585,2.82820063659975E-17,0.));
#58173=CARTESIAN_POINT('',(-0.23094010767585,2.82820063659975E-17,0.36));
#58174=CARTESIAN_POINT('Origin',(-0.115470053837925,0.2,0.));
#58175=CARTESIAN_POINT('',(-0.115470053837925,0.2,0.));
#58176=CARTESIAN_POINT('',(-0.101837567297406,0.223612159321677,0.));
#58177=CARTESIAN_POINT('',(-0.115470053837925,0.2,0.36));
#58178=CARTESIAN_POINT('',(-0.115470053837925,0.2,0.));
#58179=CARTESIAN_POINT('',(-0.115470053837925,0.2,0.36));
#58180=CARTESIAN_POINT('Origin',(0.115470053837925,0.2,0.));
#58181=CARTESIAN_POINT('',(0.115470053837925,0.2,0.));
#58182=CARTESIAN_POINT('',(0.227735026918963,0.2,0.));
#58183=CARTESIAN_POINT('',(0.115470053837925,0.2,0.36));
#58184=CARTESIAN_POINT('',(0.115470053837925,0.2,0.));
#58185=CARTESIAN_POINT('',(0.115470053837925,0.2,0.36));
#58186=CARTESIAN_POINT('Origin',(0.23094010767585,0.,0.));
#58187=CARTESIAN_POINT('',(0.23094010767585,0.,0.));
#58188=CARTESIAN_POINT('',(0.244572594216369,-0.0236121593216773,0.));
#58189=CARTESIAN_POINT('',(0.23094010767585,0.,0.36));
#58190=CARTESIAN_POINT('',(0.23094010767585,0.,0.));
#58191=CARTESIAN_POINT('',(0.23094010767585,0.,0.36));
#58192=CARTESIAN_POINT('Origin',(0.115470053837925,-0.2,0.));
#58193=CARTESIAN_POINT('',(0.186837567297406,-0.0763878406783227,0.));
#58194=CARTESIAN_POINT('',(0.115470053837925,-0.2,0.36));
#58195=CARTESIAN_POINT('Origin',(0.,0.,0.36));
#58196=CARTESIAN_POINT('Origin',(0.34,0.,0.));
#58197=CARTESIAN_POINT('',(-0.34,-4.163799117101E-17,1.73472347597681E-17));
#58198=CARTESIAN_POINT('Origin',(0.,0.,0.));
#58199=CARTESIAN_POINT('Origin',(0.,0.,0.03));
#58200=CARTESIAN_POINT('',(-0.37,-4.53119315684521E-17,0.03));
#58201=CARTESIAN_POINT('Origin',(0.,0.,0.93));
#58202=CARTESIAN_POINT('Origin',(0.,0.,1.885));
#58203=CARTESIAN_POINT('',(-0.275,-3.36777869765522E-17,1.97));
#58204=CARTESIAN_POINT('Origin',(0.,0.,1.97));
#58205=CARTESIAN_POINT('',(-0.275,-3.36777869765522E-17,1.885));
#58206=CARTESIAN_POINT('Origin',(0.,0.,1.985));
#58207=CARTESIAN_POINT('',(-0.245,-3.00038465791101E-17,2.));
#58208=CARTESIAN_POINT('Origin',(0.,0.,2.));
#58209=CARTESIAN_POINT('',(-0.26,-3.18408167778312E-17,1.985));
#58210=CARTESIAN_POINT('Origin',(0.,0.,2.));
#76630=UNCERTAINTY_MEASURE_WITH_UNIT(LENGTH_MEASURE(0.001),#76661,
'DISTANCE_ACCURACY_VALUE',
'Maximum model space distance between geometric entities at asserted c
onnectivities');
#76638=UNCERTAINTY_MEASURE_WITH_UNIT(LENGTH_MEASURE(0.001),#76661,
'DISTANCE_ACCURACY_VALUE',
'Maximum model space distance between geometric entities at asserted c
onnectivities');
#76652=(
GEOMETRIC_REPRESENTATION_CONTEXT(3)
GLOBAL_UNCERTAINTY_ASSIGNED_CONTEXT((#76630))
GLOBAL_UNIT_ASSIGNED_CONTEXT((#76661,#76663,#76664))
REPRESENTATION_CONTEXT('','3D')
);
#76660=(
GEOMETRIC_REPRESENTATION_CONTEXT(3)
GLOBAL_UNCERTAINTY_ASSIGNED_CONTEXT((#76638))
GLOBAL_UNIT_ASSIGNED_CONTEXT((#76661,#76663,#76664))
REPRESENTATION_CONTEXT('','3D')
);
#76661=(
LENGTH_UNIT()
NAMED_UNIT(*)
SI_UNIT(.CENTI.,.METRE.)
);
#76663=(
NAMED_UNIT(*)
PLANE_ANGLE_UNIT()
SI_UNIT($,.RADIAN.)
);
#76664=(
NAMED_UNIT(*)
SI_UNIT($,.STERADIAN.)
SOLID_ANGLE_UNIT()
);
#76678=SHAPE_DEFINITION_REPRESENTATION(#76699,#76748);
#76699=PRODUCT_DEFINITION_SHAPE('',$,#76770);
#76748=SHAPE_REPRESENTATION('',(#28289),#76652);
#76756=PRODUCT_DEFINITION_CONTEXT('part definition',#76821,'design');
#76770=PRODUCT_DEFINITION('2026-10-26-11-13-27-477',
'14_Quill_Guide_Screw_ISO_4028_M8x20_Dog_Point',#76791,#76756);
#76791=PRODUCT_DEFINITION_FORMATION('',$,#76836);
#76821=APPLICATION_CONTEXT(
'Core Data for Automotive Mechanical Design Process');
#76822=PRODUCT_CONTEXT('part definition',#76821,'mechanical');
#76836=PRODUCT('2026-10-26-11-13-27-477',
'14_Quill_Guide_Screw_ISO_4028_M8x20_Dog_Point',$,(#76822));
#76907=COLOUR_RGB('Black',0.12,0.14,0.17);
#76908=FILL_AREA_STYLE_COLOUR('',#76907);
#76909=FILL_AREA_STYLE('',(#76908));
#76910=SURFACE_STYLE_FILL_AREA(#76909);
#76911=SURFACE_SIDE_STYLE('',(#76910));
#76912=SURFACE_STYLE_USAGE(.BOTH.,#76911);
#76913=PRESENTATION_STYLE_ASSIGNMENT((#76912));
ENDSEC;
END-ISO-10303-21;
